ISO-10303-21;
HEADER;
FILE_DESCRIPTION (('STEP AP214'),
    '1' );
FILE_NAME ('hex flange bolt small_iso_ISO 4162 - M8 x 35 x 22-N.step',
    '2026-10-27T17:01:19',
    ( '' ),
    ( '' ),
    'SwSTEP 2.0',
    'SolidWorks 2026',
    '' );
FILE_SCHEMA (( 'AUTOMOTIVE_DESIGN' ));
ENDSEC;

DATA;
#17=CARTESIAN_POINT ( 'NONE',  ( 6.212060063025091061, 2.039954613760103896, -5.000000000000000000 ) ) ;
#20=DIRECTION ( 'NONE',  ( 0.3420201433256622736, 1.150791560227853228E-16, 0.9396926207859106484 ) ) ;
#22=B_SPLINE_CURVE_WITH_KNOTS ( 'NONE', 3,
 ( #2566, #497, #13861, #11570, #12830, #4870, #11639, #4939 ),
 .UNSPECIFIED., .F., .F.,
 ( 4, 2, 2, 4 ),
 ( 0.002921158011986709890, 0.003648658599403064012, 0.004376159186819418567, 0.005831160361652128546 ),
 .UNSPECIFIED. ) ;
#24=CARTESIAN_POINT ( 'NONE',  ( 6.244297270354683960, 1.800816419761795034E-11, 5.105276777067893512 ) ) ;
#36=ORIENTED_EDGE ( 'NONE', *, *, #12069, .F. ) ;
#48=CARTESIAN_POINT ( 'NONE',  ( 6.527192678185238961, -5.883244248022514888, -3.079566767404799650E-14 ) ) ;
#63=CARTESIAN_POINT ( 'NONE',  ( 6.244297270354684848, -1.799661607120071246E-11, -5.105276777067894400 ) ) ;
#73=B_SPLINE_CURVE_WITH_KNOTS ( 'NONE', 3,
 ( #5275, #111, #2574, #7961, #9298 ),
 .UNSPECIFIED., .F., .F.,
 ( 4, 1, 4 ),
 ( 0.000000000000000000, 0.002886751345948128985, 0.005773502691896257970 ),
 .UNSPECIFIED. ) ;
#83=ORIENTED_EDGE ( 'NONE', *, *, #7565, .F. ) ;
#106=EDGE_CURVE ( 'NONE', #2067, #2328, #1941, .T. ) ;
#111=CARTESIAN_POINT ( 'NONE',  ( 6.196878017913832970, -3.367876570272823500, -4.166666666666666963 ) ) ;
#113=CARTESIAN_POINT ( 'NONE',  ( 6.403457969954073015, -5.776886471390939803, 5.182398524903814613E-16 ) ) ;
#122=CARTESIAN_POINT ( 'NONE',  ( 6.534838248920896930, -2.951765777552407766, 5.112608298763836601 ) ) ;
#131=DIRECTION ( 'NONE',  ( 0.000000000000000000, 0.000000000000000000, 1.000000000000000000 ) ) ;
#133=SURFACE_STYLE_FILL_AREA ( #3350 ) ;
#135=ORIENTED_EDGE ( 'NONE', *, *, #9646, .T. ) ;
#136=ORIENTED_EDGE ( 'NONE', *, *, #1223, .F. ) ;
#152=CYLINDRICAL_SURFACE ( 'NONE', #12239, 4.000000000000000000 ) ;
#195=CARTESIAN_POINT ( 'NONE',  ( 6.327640840229819652, -2.033197012992983943, 4.999999999998298250 ) ) ;
#215=ORIENTED_EDGE ( 'NONE', *, *, #1697, .T. ) ;
#219=CARTESIAN_POINT ( 'NONE',  ( 6.390820841722129941, 2.823237767533145703, 5.110008744785254464 ) ) ;
#248=VERTEX_POINT ( 'NONE', #7468 ) ;
#272=CARTESIAN_POINT ( 'NONE',  ( 6.355827204229361982, 5.411702751981842141, -0.8440485055075606091 ) ) ;
#296=CARTESIAN_POINT ( 'NONE',  ( 6.095473853218515536, 3.806361898857873793, 3.407187799183811983 ) ) ;
#297=EDGE_CURVE ( 'NONE', #14514, #7459, #997, .T. ) ;
#303=CARTESIAN_POINT ( 'NONE',  ( 6.466260427357664931, 5.808561367196023006, 9.218349649774728207E-16 ) ) ;
#318=ADVANCED_FACE ( 'NONE', ( #7912 ), #1489, .F. ) ;
#329=CIRCLE ( 'NONE', #7673, 4.000000000000000000 ) ;
#341=CARTESIAN_POINT ( 'NONE',  ( 6.207541730803228575, -1.039448978216581665, 5.000000000000000888 ) ) ;
#348=CARTESIAN_POINT ( 'NONE',  ( 6.367873360227555679, -2.886751345948120662, 4.999999999999999112 ) ) ;
#353=CARTESIAN_POINT ( 'NONE',  ( -3.836423976351538233E-15, 4.452621892014634319, 2.287832656137188447 ) ) ;
#356=CARTESIAN_POINT ( 'NONE',  ( 6.495567275914603478, 2.917443832165053763, 5.053160945538326843 ) ) ;
#399=B_SPLINE_CURVE_WITH_KNOTS ( 'NONE', 3,
 ( #14537, #4512, #7899, #13513, #48, #4586, #8857, #13732, #2270, #11367, #13574, #5604, #1258, #113, #9970, #5755 ),
 .UNSPECIFIED., .F., .F.,
 ( 4, 3, 3, 3, 3, 4 ),
 ( -2.669610558405964892E-06, 0.000000000000000000, 5.703179328867167365E-05, 0.0001157653700801133104, 0.0001686517580788989934, 0.0002219032271218154611 ),
 .UNSPECIFIED. ) ;
#401=ADVANCED_FACE ( 'NONE', ( #2445 ), #4665, .T. ) ;
#427=EDGE_CURVE ( 'NONE', #5340, #2146, #5598, .T. ) ;
#428=CARTESIAN_POINT ( 'NONE',  ( 6.527192678185236296, -2.941622124011173955, 5.095038975456215091 ) ) ;
#435=CARTESIAN_POINT ( 'NONE',  ( 42.80949999999999278, 4.898587196589412829E-16, -4.000000000000000000 ) ) ;
#436=ORIENTED_EDGE ( 'NONE', *, *, #13154, .F. ) ;
#478=DIRECTION ( 'NONE',  ( -0.000000000000000000, 0.000000000000000000, 1.000000000000000000 ) ) ;
#483=VERTEX_POINT ( 'NONE', #435 ) ;
#487=CARTESIAN_POINT ( 'NONE',  ( 6.452281807715718465, 2.898928808473057117, -5.021091983800451075 ) ) ;
#497=CARTESIAN_POINT ( 'NONE',  ( -8.271276729938239853E-16, -4.452621892014642313, -2.287832656137187115 ) ) ;
#500=CARTESIAN_POINT ( 'NONE',  ( 0.000000000000000000, -4.330127018922189208, 2.500000000000010658 ) ) ;
#521=AXIS2_PLACEMENT_3D ( 'NONE', #8840, #3304, #12297 ) ;
#544=EDGE_CURVE ( 'NONE', #1949, #5340, #2948, .T. ) ;
#573=ORIENTED_EDGE ( 'NONE', *, *, #7330, .T. ) ;
#591=EDGE_CURVE ( 'NONE', #9255, #483, #329, .T. ) ;
#592=CARTESIAN_POINT ( 'NONE',  ( 0.000000000000000000, 0.000000000000000000, 5.000000000000000888 ) ) ;
#595=UNCERTAINTY_MEASURE_WITH_UNIT (LENGTH_MEASURE( 1.000000000000000082E-05 ), #7441, 'distance_accuracy_value', 'NONE');
#609=CARTESIAN_POINT ( 'NONE',  ( 0.3117969352650125092, 2.419842229202151529, -4.999999999999999112 ) ) ;
#616=ORIENTED_EDGE ( 'NONE', *, *, #591, .T. ) ;
#621=B_SPLINE_CURVE_WITH_KNOTS ( 'NONE', 3,
 ( #11192, #10162, #7940, #12294, #4630, #24 ),
 .UNSPECIFIED., .F., .F.,
 ( 4, 2, 4 ),
 ( 0.000000000000000000, 0.001488912493401912647, 0.002977824986803825295 ),
 .UNSPECIFIED. ) ;
#632=VECTOR ( 'NONE', #8279, 1000.000000000000000 ) ;
#641=ORIENTED_EDGE ( 'NONE', *, *, #544, .T. ) ;
#653=PLANE ( 'NONE',  #2277 ) ;
#693=CARTESIAN_POINT ( 'NONE',  ( 0.000000000000000000, 0.000000000000000000, 4.000000000000000000 ) ) ;
#718=( NAMED_UNIT ( * ) SI_UNIT ( $, .STERADIAN. ) SOLID_ANGLE_UNIT ( ) );
#723=AXIS2_PLACEMENT_3D ( 'NONE', #11252, #12424, #13480 ) ;
#737=PRODUCT_CONTEXT ( 'NONE', #1226, 'mechanical' ) ;
#763=DIRECTION ( 'NONE',  ( 0.000000000000000000, 0.000000000000000000, -1.000000000000000000 ) ) ;
#803=CARTESIAN_POINT ( 'NONE',  ( 6.367873360227558344, -2.886751345948134873, -5.000000000000000000 ) ) ;
#832=CARTESIAN_POINT ( 'NONE',  ( 6.092449800118089343, -3.827241605637789590, 3.371023086193853047 ) ) ;
#841=FACE_OUTER_BOUND ( 'NONE', #13446, .T. ) ;
#855=ORIENTED_EDGE ( 'NONE', *, *, #12978, .T. ) ;
#895=CARTESIAN_POINT ( 'NONE',  ( 7.336184427528458230, 0.000000000000000000, 0.000000000000000000 ) ) ;
#903=EDGE_LOOP ( 'NONE', ( #641, #14232, #14441 ) ) ;
#925=CARTESIAN_POINT ( 'NONE',  ( 0.000000000000000000, 4.898587196589412829E-16, -4.000000000000000000 ) ) ;
#935=EDGE_CURVE ( 'NONE', #14514, #6201, #5231, .T. ) ;
#948=CARTESIAN_POINT ( 'NONE',  ( 8.500000000000000000, 2.886751345948125547, 4.999999999999999112 ) ) ;
#956=B_SPLINE_CURVE_WITH_KNOTS ( 'NONE', 3,
 ( #12612, #7154, #2877, #2657, #2946, #11868 ),
 .UNSPECIFIED., .F., .F.,
 ( 4, 2, 4 ),
 ( 4.336808689942017736E-19, 0.001488912493401923489, 0.002977824986803846545 ),
 .UNSPECIFIED. ) ;
#963=CARTESIAN_POINT ( 'NONE',  ( 0.000000000000000000, 0.000000000000000000, 0.000000000000000000 ) ) ;
#997=CIRCLE ( 'NONE', #9256, 5.000000000000000000 ) ;
#1023=ADVANCED_FACE ( 'NONE', ( #11243 ), #10558, .T. ) ;
#1035=ORIENTED_EDGE ( 'NONE', *, *, #8104, .F. ) ;
#1041=CARTESIAN_POINT ( 'NONE',  ( 6.367873360227556567, 2.886751345948125547, 4.999999999999999112 ) ) ;
#1060=DIRECTION ( 'NONE',  ( 0.000000000000000000, -0.5000000000000012212, -0.8660254037844380415 ) ) ;
#1103=DIRECTION ( 'NONE',  ( 1.000000000000000000, 0.000000000000000000, -0.000000000000000000 ) ) ;
#1109=( NAMED_UNIT ( * ) PLANE_ANGLE_UNIT ( ) SI_UNIT ( $, .RADIAN. ) );
#1117=DIRECTION ( 'NONE',  ( -1.000000000000000000, -0.000000000000000000, -0.000000000000000000 ) ) ;
#1137=CARTESIAN_POINT ( 'NONE',  ( 6.323268674612417151, -2.010012106700867385, -5.000000000000872191 ) ) ;
#1143=ORIENTED_EDGE ( 'NONE', *, *, #9016, .T. ) ;
#1166=CARTESIAN_POINT ( 'NONE',  ( 7.336184427528458230, 9.926022037524705097E-16, 8.105212085995399107 ) ) ;
#1173=CONICAL_SURFACE ( 'NONE', #6364, 8.105212085995399107, 1.221730476396037490 ) ;
#1188=CARTESIAN_POINT ( 'NONE',  ( 6.534838248920896930, 2.951765777552409986, -5.112608298763837489 ) ) ;
#1209=CARTESIAN_POINT ( 'NONE',  ( 6.506987859255520590, 5.850751062354591525, -2.486036146584983242E-15 ) ) ;
#1216=CARTESIAN_POINT ( 'NONE',  ( 0.000000000000000000, 0.000000000000000000, 0.000000000000000000 ) ) ;
#1219=CARTESIAN_POINT ( 'NONE',  ( 6.390983168987730778, -3.014662706507984513, -5.000000000000000000 ) ) ;
#1223=EDGE_CURVE ( 'NONE', #11111, #2958, #8567, .T. ) ;
#1226=APPLICATION_CONTEXT ( 'automotive_design' ) ;
#1230=CARTESIAN_POINT ( 'NONE',  ( 0.1996310553826622369, 1.947030205581111728, 4.999999999999997335 ) ) ;
#1258=CARTESIAN_POINT ( 'NONE',  ( 6.420058897733094128, -5.782965130189197112, 5.182398524903814613E-16 ) ) ;
#1268=CARTESIAN_POINT ( 'NONE',  ( 6.242800618755250497, -4.918813924287368522, -1.690830708135581784 ) ) ;
#1276=ORIENTED_EDGE ( 'NONE', *, *, #5646, .T. ) ;
#1279=CARTESIAN_POINT ( 'NONE',  ( 7.900000000000002132, 9.674709713264094059E-16, -7.900000000000002132 ) ) ;
#1283=FACE_OUTER_BOUND ( 'NONE', #8141, .T. ) ;
#1330=CARTESIAN_POINT ( 'NONE',  ( 6.452281807715718465, -2.898928808473054897, 5.021091983800450187 ) ) ;
#1332=CARTESIAN_POINT ( 'NONE',  ( 6.207671477328849718, -5.338259717474132415, -0.7538629453365324196 ) ) ;
#1336=CARTESIAN_POINT ( 'NONE',  ( 43.50000000000000711, 0.000000000000000000, 0.000000000000000000 ) ) ;
#1359=CARTESIAN_POINT ( 'NONE',  ( 6.092460485788117275, -1.005982284677391592, -5.000000000000000000 ) ) ;
#1362=LINE ( 'NONE', #8222, #5207 ) ;
#1386=CARTESIAN_POINT ( 'NONE',  ( -4.726443845678993920E-16, -0.4883827417527498160, -4.999999999999999112 ) ) ;
#1392=CARTESIAN_POINT ( 'NONE',  ( 6.518095160332179283, 2.933089652807376435, -5.080260301816947432 ) ) ;
#1403=AXIS2_PLACEMENT_3D ( 'NONE', #13360, #13522, #12174 ) ;
#1408=ORIENTED_EDGE ( 'NONE', *, *, #1824, .F. ) ;
#1422=CARTESIAN_POINT ( 'NONE',  ( 6.362374563307939823, 3.415000007733389076, 4.302769906042884784 ) ) ;
#1439=AXIS2_PLACEMENT_3D ( 'NONE', #6477, #11186, #12285 ) ;
#1442=EDGE_LOOP ( 'NONE', ( #2693, #5441, #7947, #6102 ) ) ;
#1443=CARTESIAN_POINT ( 'NONE',  ( 6.095462721915160920, 1.047438013716504246, -5.000000000000000000 ) ) ;
#1466=CARTESIAN_POINT ( 'NONE',  ( 0.1739375980333730809, 5.301268757141563093, -0.8179331680533001858 ) ) ;
#1472=CARTESIAN_POINT ( 'NONE',  ( 8.500000000000000000, 0.000000000000000000, 0.000000000000000000 ) ) ;
#1489=( BOUNDED_SURFACE ( )  B_SPLINE_SURFACE ( 3, 2, ( 
 ( #9088, #4599, #13588 ),
 ( #4442, #11378, #4753 ),
 ( #10202, #6876, #5619 ),
 ( #7975, #6725, #1268 ),
 ( #1332, #5547, #11298 ),
 ( #10119, #2368, #3478 ) ),
 .UNSPECIFIED., .F., .F., .F. ) 
 B_SPLINE_SURFACE_WITH_KNOTS ( ( 4, 2, 4 ),
 ( 3, 3 ),
 ( 0.02367865728600892367, 0.02663179453327098323, 0.02958493178053304279 ),
 ( 0.000000000000000000, 1.000000000000000000 ),
 .UNSPECIFIED. ) 
 GEOMETRIC_REPRESENTATION_ITEM ( )  RATIONAL_B_SPLINE_SURFACE ( (
 ( 1.000000000000000000, 0.8047781103519396906, 1.000000000000000000),
 ( 1.000000000000000000, 0.8123785825973208752, 1.000000000000000000),
 ( 1.000000000000000000, 0.8190671539297160741, 1.000000000000000000),
 ( 1.000000000000000000, 0.8192352255325974220, 1.000000000000000000),
 ( 1.000000000000000000, 0.8126129676842738236, 1.000000000000000000),
 ( 1.000000000000000000, 0.8047712537969737845, 1.000000000000000000) ) ) 
 REPRESENTATION_ITEM ( '' )  SURFACE ( )  );
#1536=CARTESIAN_POINT ( 'NONE',  ( 0.4465819873851989974, -2.886751345948121106, 4.999999999999999112 ) ) ;
#1540=CARTESIAN_POINT ( 'NONE',  ( 6.244889965166094292, 4.918546365148221078, -1.691415889817840412 ) ) ;
#1565=CARTESIAN_POINT ( 'NONE',  ( 6.495567275914606142, -2.917443832165063533, -5.053160945538327731 ) ) ;
#1663=CARTESIAN_POINT ( 'NONE',  ( 8.500000000000000000, 9.800365875394399578E-16, -7.900000000000002132 ) ) ;
#1677=CARTESIAN_POINT ( 'NONE',  ( 6.420058897733097680, 2.891482565094590562, -5.008194711943424693 ) ) ;
#1696=ADVANCED_FACE ( 'NONE', ( #6187 ), #9866, .T. ) ;
#1697=EDGE_CURVE ( 'NONE', #9831, #3784, #6454, .T. ) ;
#1710=FACE_OUTER_BOUND ( 'NONE', #14218, .T. ) ;
#1715=EDGE_LOOP ( 'NONE', ( #3495, #11886, #10893, #12501, #10491 ) ) ;
#1736=CARTESIAN_POINT ( 'NONE',  ( 0.4465819873851995525, 2.886751345948122882, -5.000000000000000000 ) ) ;
#1738=ORIENTED_EDGE ( 'NONE', *, *, #7077, .F. ) ;
#1743=ORIENTED_EDGE ( 'NONE', *, *, #13399, .T. ) ;
#1747=CARTESIAN_POINT ( 'NONE',  ( 6.367873360227556567, 2.886751345948125547, 4.999999999999999112 ) ) ;
#1765=EDGE_CURVE ( 'NONE', #11111, #7982, #8342, .T. ) ;
#1781=DIRECTION ( 'NONE',  ( 1.000000000000000000, 0.000000000000000000, 0.000000000000000000 ) ) ;
#1787=FACE_OUTER_BOUND ( 'NONE', #14245, .T. ) ;
#1790=CARTESIAN_POINT ( 'NONE',  ( 43.50000000000000711, 0.000000000000000000, 3.309499999999999886 ) ) ;
#1793=CARTESIAN_POINT ( 'NONE',  ( 8.500000000000000000, 5.773502691896261751, 0.000000000000000000 ) ) ;
#1800=ORIENTED_EDGE ( 'NONE', *, *, #6923, .F. ) ;
#1801=CARTESIAN_POINT ( 'NONE',  ( 6.390983399715590707, -2.822795037344613789, 5.110775575965826434 ) ) ;
#1814=B_SPLINE_CURVE_WITH_KNOTS ( 'NONE', 3,
 ( #5921, #14043, #11728, #6143, #10425, #12705, #13816, #12784, #356, #13892, #2676, #3712, #8193, #2600, #3927, #7098 ),
 .UNSPECIFIED., .F., .F.,
 ( 4, 3, 3, 3, 3, 4 ),
 ( 0.000000000000000000, 5.303647860849296453E-05, 0.0001057093501027513691, 0.0001642058037233857007, 0.0002210073443967692478, 0.0002236769549551747692 ),
 .UNSPECIFIED. ) ;
#1816=DIRECTION ( 'NONE',  ( 0.000000000000000000, 0.000000000000000000, 1.000000000000000000 ) ) ;
#1824=EDGE_CURVE ( 'NONE', #9269, #7982, #8456, .T. ) ;
#1849=ADVANCED_FACE ( 'NONE', ( #10641 ), #653, .F. ) ;
#1852=CIRCLE ( 'NONE', #2573, 5.000000000000000000 ) ;
#1874=ADVANCED_FACE ( 'NONE', ( #6352 ), #6796, .T. ) ;
#1907=CARTESIAN_POINT ( 'NONE',  ( 6.355827204229362870, 3.436818823786758070, 4.264647808192652434 ) ) ;
#1934=COLOUR_RGB ( '',1.000000000000000000, 0.9490196078431372140, 0.9098039215686274384 ) ;
#1941=CIRCLE ( 'NONE', #11374, 7.900000000000002132 ) ;
#1949=VERTEX_POINT ( 'NONE', #4078 ) ;
#1952=EDGE_CURVE ( 'NONE', #12984, #14237, #14267, .T. ) ;
#1972=CARTESIAN_POINT ( 'NONE',  ( 0.1973348417602471538, -1.936114729415142399, 4.999999999999999112 ) ) ;
#1984=EDGE_LOOP ( 'NONE', ( #1143, #10346, #3079 ) ) ;
#1992=CARTESIAN_POINT ( 'NONE',  ( 6.270568613849416550, -4.911887854652846386, -1.704496029161937987 ) ) ;
#2006=EDGE_LOOP ( 'NONE', ( #3942, #13481, #136, #9943 ) ) ;
#2015=CARTESIAN_POINT ( 'NONE',  ( 6.207671477327360243, -3.321994320370016407, 4.246137054663877919 ) ) ;
#2045=EDGE_CURVE ( 'NONE', #9831, #248, #3401, .T. ) ;
#2067=VERTEX_POINT ( 'NONE', #9142 ) ;
#2094=DIRECTION ( 'NONE',  ( 0.000000000000000000, -0.8660254037844380415, 0.5000000000000012212 ) ) ;
#2112=ORIENTED_EDGE ( 'NONE', *, *, #12312, .T. ) ;
#2131=CARTESIAN_POINT ( 'NONE',  ( 6.196878017913830305, 1.924500897298746738, -4.999999999999999112 ) ) ;
#2146=VERTEX_POINT ( 'NONE', #4812 ) ;
#2164=EDGE_CURVE ( 'NONE', #3784, #2958, #10926, .T. ) ;
#2175=B_SPLINE_CURVE_WITH_KNOTS ( 'NONE', 3,
 ( #9844, #5345, #14346, #7779, #5495, #11094, #12055, #14279 ),
 .UNSPECIFIED., .F., .F.,
 ( 4, 2, 2, 4 ),
 ( 0.002921158011986723334, 0.003648658599403076588, 0.004376159186819428976, 0.005831160361652135485 ),
 .UNSPECIFIED. ) ;
#2189=CARTESIAN_POINT ( 'NONE',  ( 6.196878017913830305, -1.924500897298746072, 4.999999999999999112 ) ) ;
#2230=FACE_OUTER_BOUND ( 'NONE', #4194, .T. ) ;
#2243=CARTESIAN_POINT ( 'NONE',  ( 6.242811304425486263, -0.9953138271156629635, -5.105233480330447549 ) ) ;
#2266=DIRECTION ( 'NONE',  ( 0.000000000000000000, 0.000000000000000000, 1.000000000000000000 ) ) ;
#2270=CARTESIAN_POINT ( 'NONE',  ( 6.481779955677548166, -5.820445026626441809, 3.602012395189916580E-16 ) ) ;
#2277=AXIS2_PLACEMENT_3D ( 'NONE', #948, #6650, #11942 ) ;
#2302=CARTESIAN_POINT ( 'NONE',  ( 6.385552186430389021, 5.773502691896261751, 0.000000000000000000 ) ) ;
#2317=EDGE_LOOP ( 'NONE', ( #855, #1800, #4859, #11102 ) ) ;
#2322=ORIENTED_EDGE ( 'NONE', *, *, #1223, .T. ) ;
#2328=VERTEX_POINT ( 'NONE', #1663 ) ;
#2343=VECTOR ( 'NONE', #10076, 1000.000000000000000 ) ;
#2347=DIRECTION ( 'NONE',  ( -0.7071067811865530128, 8.659560562354868763E-17, -0.7071067811865421326 ) ) ;
#2349=ORIENTED_EDGE ( 'NONE', *, *, #4390, .F. ) ;
#2351=CARTESIAN_POINT ( 'NONE',  ( 7.336184427528458230, 0.000000000000000000, -8.105212085995399107 ) ) ;
#2368=CARTESIAN_POINT ( 'NONE',  ( 6.507056315241516842, -5.826803161468475878, 0.09231912136634906618 ) ) ;
#2373=( LENGTH_UNIT ( ) NAMED_UNIT ( * ) SI_UNIT ( .MILLI., .METRE. ) );
#2385=CARTESIAN_POINT ( 'NONE',  ( 6.327632967270169217, 5.346704644971289611, -0.7392359018470683329 ) ) ;
#2391=CARTESIAN_POINT ( 'NONE',  ( 6.367873360227558344, 5.773502691896261751, 0.000000000000000000 ) ) ;
#2418=CARTESIAN_POINT ( 'NONE',  ( 5.991014884144047592, -4.330127018922192761, 2.499999999999998668 ) ) ;
#2445=FACE_OUTER_BOUND ( 'NONE', #903, .T. ) ;
#2458=ORIENTED_EDGE ( 'NONE', *, *, #4543, .T. ) ;
#2459=DIRECTION ( 'NONE',  ( -1.000000000000000000, -0.000000000000000000, -0.000000000000000000 ) ) ;
#2466=DIRECTION ( 'NONE',  ( 0.000000000000000000, 0.000000000000000000, -1.000000000000000000 ) ) ;
#2489=B_SPLINE_CURVE_WITH_KNOTS ( 'NONE', 3,
 ( #1736, #609, #10590, #14004, #14066, #6090 ),
 .UNSPECIFIED., .F., .F.,
 ( 4, 2, 4 ),
 ( 0.01506847346324403751, 0.01653041426658208995, 0.01799235506992014066 ),
 .UNSPECIFIED. ) ;
#2499=CARTESIAN_POINT ( 'NONE',  ( 6.507056549636238252, 2.993353539201077496, 4.999999999999999112 ) ) ;
#2519=CARTESIAN_POINT ( 'NONE',  ( 6.327632967268630004, 3.313549392874629795, 4.260764098153893897 ) ) ;
#2520=B_SPLINE_CURVE_WITH_KNOTS ( 'NONE', 3,
 ( #6658, #5694, #9015, #6869, #12552 ),
 .UNSPECIFIED., .F., .F.,
 ( 4, 1, 4 ),
 ( 0.000000000000000000, 0.002886751345948132454, 0.005773502691896264909 ),
 .UNSPECIFIED. ) ;
#2530=CARTESIAN_POINT ( 'NONE',  ( 6.534224484704354907, 5.901860969583193395, 3.353103961394464287E-14 ) ) ;
#2566=CARTESIAN_POINT ( 'NONE',  ( 0.000000000000000000, -4.330127018922194537, -2.500000000000000444 ) ) ;
#2568=DIRECTION ( 'NONE',  ( 0.000000000000000000, 0.000000000000000000, 1.000000000000000000 ) ) ;
#2572=CONICAL_SURFACE ( 'NONE', #1403, 3.309499999999999886, 0.7853981633974407295 ) ;
#2573=AXIS2_PLACEMENT_3D ( 'NONE', #13352, #3464, #12457 ) ;
#2574=CARTESIAN_POINT ( 'NONE',  ( 5.991014884144049368, -4.330127018922198978, -2.500000000000000444 ) ) ;
#2577=CARTESIAN_POINT ( 'NONE',  ( 6.242789945155967857, 0.9948955795114693412, 5.105232858000414708 ) ) ;
#2592=CARTESIAN_POINT ( 'NONE',  ( 0.000000000000000000, 0.000000000000000000, 0.000000000000000000 ) ) ;
#2600=CARTESIAN_POINT ( 'NONE',  ( 6.534224484704352243, 2.950930484791584263, 5.111161529262904679 ) ) ;
#2613=AXIS2_PLACEMENT_3D ( 'NONE', #11424, #3458, #2266 ) ;
#2642=CARTESIAN_POINT ( 'NONE',  ( -3.761337442881754015E-15, 3.838309248099015747, 3.351853367131007122 ) ) ;
#2644=CIRCLE ( 'NONE', #12059, 5.000000000000000000 ) ;
#2657=CARTESIAN_POINT ( 'NONE',  ( 6.271006797790669829, -0.9853839345309193254, -5.106080050406711202 ) ) ;
#2659=CARTESIAN_POINT ( 'NONE',  ( 6.204449577088272605, 0.9975080636026212311, 5.000000000000000000 ) ) ;
#2669=DIRECTION ( 'NONE',  ( 0.000000000000000000, 0.000000000000000000, -1.000000000000000000 ) ) ;
#2676=CARTESIAN_POINT ( 'NONE',  ( 6.518095160332174842, 2.933089652807376435, 5.080260301816937663 ) ) ;
#2687=CARTESIAN_POINT ( 'NONE',  ( 6.481779955677546390, -2.910222513313224457, -5.040653254389286353 ) ) ;
#2692=FACE_OUTER_BOUND ( 'NONE', #10073, .T. ) ;
#2693=ORIENTED_EDGE ( 'NONE', *, *, #3278, .F. ) ;
#2699=DIRECTION ( 'NONE',  ( 1.000000000000000000, 0.000000000000000000, 0.000000000000000000 ) ) ;
#2701=VERTEX_POINT ( 'NONE', #11931 ) ;
#2704=CARTESIAN_POINT ( 'NONE',  ( 6.445127866599364985, -3.194847394660945916, 4.687657648742338701 ) ) ;
#2746=CARTESIAN_POINT ( 'NONE',  ( 6.534224484704354907, -2.950930484791607800, -5.111161529262896686 ) ) ;
#2763=DIRECTION ( 'NONE',  ( 0.000000000000000000, 0.000000000000000000, -1.000000000000000000 ) ) ;
#2771=CARTESIAN_POINT ( 'NONE',  ( 6.355827204229362870, -5.411702751981846582, 0.8440485055075603871 ) ) ;
#2777=CARTESIAN_POINT ( 'NONE',  ( 6.506987859255528583, 2.925375531177293986, -5.066899051217878203 ) ) ;
#2778=CIRCLE ( 'NONE', #7251, 8.105212085995399107 ) ;
#2805=AXIS2_PLACEMENT_3D ( 'NONE', #1279, #7859, #7780 ) ;
#2811=CARTESIAN_POINT ( 'NONE',  ( 8.500000000000000000, 2.886751345948122882, -5.000000000000000000 ) ) ;
#2877=CARTESIAN_POINT ( 'NONE',  ( 6.371919382990606451, -1.972754410575520367, -5.108792907957607099 ) ) ;
#2895=CARTESIAN_POINT ( 'NONE',  ( 0.000000000000000000, 4.330127018922191873, 2.500000000000005773 ) ) ;
#2917=PLANE ( 'NONE',  #8480 ) ;
#2926=ORIENTED_EDGE ( 'NONE', *, *, #10772, .T. ) ;
#2934=CARTESIAN_POINT ( 'NONE',  ( 6.534533895392293346, 2.951347675328718001, -5.111884124469663782 ) ) ;
#2946=CARTESIAN_POINT ( 'NONE',  ( 6.244297270355322560, -0.4917101305082268725, -5.105276777067913052 ) ) ;
#2948=B_SPLINE_CURVE_WITH_KNOTS ( 'NONE', 3,
 ( #3705, #6137, #10555, #12777 ),
 .UNSPECIFIED., .F., .F.,
 ( 4, 4 ),
 ( 2.380735200832039115E-07, 0.002921158011986728538 ),
 .UNSPECIFIED. ) ;
#2958=VERTEX_POINT ( 'NONE', #11271 ) ;
#2964=ORIENTED_EDGE ( 'NONE', *, *, #6483, .T. ) ;
#2966=ORIENTED_EDGE ( 'NONE', *, *, #1697, .F. ) ;
#3016=CARTESIAN_POINT ( 'NONE',  ( 6.244004651191001010, 4.663678638742294602, 2.132808149174402867 ) ) ;
#3030=VECTOR ( 'NONE', #5918, 1000.000000000000000 ) ;
#3034=SHAPE_DEFINITION_REPRESENTATION ( #14411, #9337 ) ;
#3065=VERTEX_POINT ( 'NONE', #1747 ) ;
#3079=ORIENTED_EDGE ( 'NONE', *, *, #297, .T. ) ;
#3109=ORIENTED_EDGE ( 'NONE', *, *, #2045, .F. ) ;
#3144=ORIENTED_EDGE ( 'NONE', *, *, #2045, .T. ) ;
#3146=CARTESIAN_POINT ( 'NONE',  ( 6.212068001623118008, -5.350125758160992007, 0.7333103599822092811 ) ) ;
#3161=CARTESIAN_POINT ( 'NONE',  ( -9.232659125071873696E-16, -0.4883827417527039638, 4.999999999999999112 ) ) ;
#3208=CARTESIAN_POINT ( 'NONE',  ( 6.245824673232968749, -4.939548505212512097, 1.655093584846542454 ) ) ;
#3221=CYLINDRICAL_SURFACE ( 'NONE', #4997, 4.000000000000000000 ) ;
#3277=CARTESIAN_POINT ( 'NONE',  ( 8.500000000000000000, 5.773502691896261751, -2.749426538070115714E-16 ) ) ;
#3278=EDGE_CURVE ( 'NONE', #2328, #248, #11283, .T. ) ;
#3297=CARTESIAN_POINT ( 'NONE',  ( 0.04201760816083372624, -0.9730571234388146751, 4.999999999999997335 ) ) ;
#3304=DIRECTION ( 'NONE',  ( -1.000000000000000000, -0.000000000000000000, -0.000000000000000000 ) ) ;
#3350=FILL_AREA_STYLE ('',( #13530 ) ) ;
#3359=CIRCLE ( 'NONE', #12298, 7.900000000000002132 ) ;
#3386=ORIENTED_EDGE ( 'NONE', *, *, #1824, .T. ) ;
#3388=ORIENTED_EDGE ( 'NONE', *, *, #3766, .F. ) ;
#3401=LINE ( 'NONE', #2351, #13616 ) ;
#3402=CARTESIAN_POINT ( 'NONE',  ( 6.367873360227556567, 2.886751345948122882, -5.000000000000000000 ) ) ;
#3418=ORIENTED_EDGE ( 'NONE', *, *, #297, .F. ) ;
#3441=DIRECTION ( 'NONE',  ( -1.000000000000000000, -0.000000000000000000, 0.000000000000000000 ) ) ;
#3447=ADVANCED_FACE ( 'NONE', ( #9478 ), #7520, .F. ) ;
#3458=DIRECTION ( 'NONE',  ( -1.000000000000000000, -0.000000000000000000, -0.000000000000000000 ) ) ;
#3464=DIRECTION ( 'NONE',  ( 1.000000000000000000, 0.000000000000000000, -0.000000000000000000 ) ) ;
#3476=CARTESIAN_POINT ( 'NONE',  ( 6.534838248920896930, -2.951765777552407766, 5.112608298763836601 ) ) ;
#3478=CARTESIAN_POINT ( 'NONE',  ( 6.541334219041339715, -5.921300567812619597, 0.03049376373817746025 ) ) ;
#3485=CARTESIAN_POINT ( 'NONE',  ( 6.367873360227558344, 5.773502691896261751, 0.000000000000000000 ) ) ;
#3493=CARTESIAN_POINT ( 'NONE',  ( 6.541171661047877173, 5.920857802016177729, 0.02973393389965222483 ) ) ;
#3495=ORIENTED_EDGE ( 'NONE', *, *, #6109, .F. ) ;
#3504=CARTESIAN_POINT ( 'NONE',  ( 0.000000000000000000, 0.000000000000000000, 0.000000000000000000 ) ) ;
#3548=CONICAL_SURFACE ( 'NONE', #11543, 5.000000000000000888, 1.047197551196600296 ) ;
#3555=CARTESIAN_POINT ( 'NONE',  ( 6.466260427357672924, -2.904280683598006618, 5.030361703432631337 ) ) ;
#3592=ADVANCED_FACE ( 'NONE', ( #9084 ), #2572, .T. ) ;
#3593=MECHANICAL_DESIGN_GEOMETRIC_PRESENTATION_REPRESENTATION('',(#11352),#11822);
#3595=ORIENTED_EDGE ( 'NONE', *, *, #11330, .T. ) ;
#3597=B_SPLINE_CURVE_WITH_KNOTS ( 'NONE', 3,
 ( #1041, #10048, #11231, #10208, #3485 ),
 .UNSPECIFIED., .F., .F.,
 ( 4, 1, 4 ),
 ( 0.000000000000000000, 0.002886751345948130286, 0.005773502691896260572 ),
 .UNSPECIFIED. ) ;
#3603=ORIENTED_EDGE ( 'NONE', *, *, #4495, .T. ) ;
#3616=CARTESIAN_POINT ( 'NONE',  ( 0.000000000000000000, 4.330127018922190985, -2.500000000000007105 ) ) ;
#3636=CARTESIAN_POINT ( 'NONE',  ( 6.518095160332178395, -2.933089652807374215, 5.080260301816945656 ) ) ;
#3650=CARTESIAN_POINT ( 'NONE',  ( 6.506891779418573662, 2.833891091414751706, 5.091556646552823473 ) ) ;
#3654=DIRECTION ( 'NONE',  ( 0.000000000000000000, 0.000000000000000000, -1.000000000000000000 ) ) ;
#3656=CARTESIAN_POINT ( 'NONE',  ( 6.420058897733093239, 5.782965130189193559, -4.012520129335570115E-16 ) ) ;
#3662=ORIENTED_EDGE ( 'NONE', *, *, #6345, .F. ) ;
#3664=CARTESIAN_POINT ( 'NONE',  ( 6.541333988313477121, -2.987057409892287740, -5.112749828287758369 ) ) ;
#3667=VERTEX_POINT ( 'NONE', #3476 ) ;
#3674=CARTESIAN_POINT ( 'NONE',  ( 0.4465819873851997746, 2.886751345948125547, 4.999999999999999112 ) ) ;
#3705=CARTESIAN_POINT ( 'NONE',  ( 0.4465819873852049926, -5.773502691896264416, 5.911082023588295771E-17 ) ) ;
#3712=CARTESIAN_POINT ( 'NONE',  ( 6.527192678185236296, 2.941622124011284978, 5.095038975456149366 ) ) ;
#3718=CARTESIAN_POINT ( 'NONE',  ( 6.092449800118089343, 4.833012432206481357, 1.628976913806340798 ) ) ;
#3766=EDGE_CURVE ( 'NONE', #8256, #3667, #5494, .T. ) ;
#3770=FACE_OUTER_BOUND ( 'NONE', #10780, .T. ) ;
#3784=VERTEX_POINT ( 'NONE', #7163 ) ;
#3797=CARTESIAN_POINT ( 'NONE',  ( 8.500000000000000000, -2.886751345948120662, 4.999999999999999112 ) ) ;
#3806=CARTESIAN_POINT ( 'NONE',  ( 6.533910050139697390, -2.950514251728070469, -5.110440592449064567 ) ) ;
#3822=FACE_OUTER_BOUND ( 'NONE', #6084, .T. ) ;
#3827=CARTESIAN_POINT ( 'NONE',  ( 6.534838248920900483, -5.903531555104837736, 5.201568163584232486E-16 ) ) ;
#3842=CARTESIAN_POINT ( 'NONE',  ( 0.08165819712376755357, -3.720292241887083851, 3.556264818047238929 ) ) ;
#3863=LINE ( 'NONE', #8272, #3030 ) ;
#3879=CARTESIAN_POINT ( 'NONE',  ( 6.367873360227558344, -2.886751345948134873, -5.000000000000000000 ) ) ;
#3884=ORIENTED_EDGE ( 'NONE', *, *, #4475, .F. ) ;
#3899=CARTESIAN_POINT ( 'NONE',  ( 0.1739375980333716654, 3.358985280702821097, 4.182066831946702479 ) ) ;
#3900=CARTESIAN_POINT ( 'NONE',  ( 6.436591462021373999, 2.894509378375945019, -5.013437306331756105 ) ) ;
#3927=CARTESIAN_POINT ( 'NONE',  ( 6.534533895392294234, 2.951347675328725106, 5.111884124469659341 ) ) ;
#3928=ORIENTED_EDGE ( 'NONE', *, *, #12978, .F. ) ;
#3936=CARTESIAN_POINT ( 'NONE',  ( 6.367873360227558344, -2.886751345948134873, -5.000000000000000000 ) ) ;
#3942=ORIENTED_EDGE ( 'NONE', *, *, #8104, .T. ) ;
#3989=CARTESIAN_POINT ( 'NONE',  ( 6.541334219041336162, 2.934241909852038699, -5.143243597038031467 ) ) ;
#4011=VECTOR ( 'NONE', #6688, 1000.000000000000000 ) ;
#4015=DIRECTION ( 'NONE',  ( 1.000000000000000000, 0.000000000000000000, 0.000000000000000000 ) ) ;
#4056=FACE_OUTER_BOUND ( 'NONE', #12606, .T. ) ;
#4059=PRODUCT_DEFINITION ( 'UNKNOWN', '', #5954, #13137 ) ;
#4067=ADVANCED_BREP_SHAPE_REPRESENTATION ( '', ( #7073, #9440 ), #7588 ) ;
#4072=CARTESIAN_POINT ( 'NONE',  ( 6.245824673232968749, 4.939548505212512097, -1.655093584846542010 ) ) ;
#4078=CARTESIAN_POINT ( 'NONE',  ( 0.4465819873852049926, -5.773502691896264416, 5.911082023588295771E-17 ) ) ;
#4090=CARTESIAN_POINT ( 'NONE',  ( 6.357976367241986893, 5.421935536069748096, 0.8264656814052228073 ) ) ;
#4091=B_SPLINE_CURVE_WITH_KNOTS ( 'NONE', 3,
 ( #11565, #1466, #5967, #3616 ),
 .UNSPECIFIED., .F., .F.,
 ( 4, 4 ),
 ( 2.380735200834041289E-07, 0.002921158011986723334 ),
 .UNSPECIFIED. ) ;
#4094=ORIENTED_EDGE ( 'NONE', *, *, #10616, .F. ) ;
#4112=FACE_OUTER_BOUND ( 'NONE', #9187, .T. ) ;
#4118=FACE_OUTER_BOUND ( 'NONE', #11843, .T. ) ;
#4144=CARTESIAN_POINT ( 'NONE',  ( 5.991014884144048480, -5.637851296924623057E-15, -5.000000000000000000 ) ) ;
#4147=EDGE_CURVE ( 'NONE', #7982, #7459, #4091, .T. ) ;
#4163=( LENGTH_UNIT ( ) NAMED_UNIT ( * ) SI_UNIT ( .MILLI., .METRE. ) );
#4177=EDGE_LOOP ( 'NONE', ( #3386, #7778, #5979 ) ) ;
#4180=ORIENTED_EDGE ( 'NONE', *, *, #11512, .F. ) ;
#4183=ORIENTED_EDGE ( 'NONE', *, *, #11310, .T. ) ;
#4194=EDGE_LOOP ( 'NONE', ( #13696, #8382, #2322, #7933 ) ) ;
#4205=CARTESIAN_POINT ( 'NONE',  ( 6.095473853218515536, 4.853892138986622307, -1.592812200815997059 ) ) ;
#4215=CARTESIAN_POINT ( 'NONE',  ( 6.367873360227556567, 2.886751345948122882, -5.000000000000000000 ) ) ;
#4216=CARTESIAN_POINT ( 'NONE',  ( 6.534838248920900483, -5.903531555104837736, 5.201568163584232486E-16 ) ) ;
#4223=CARTESIAN_POINT ( 'NONE',  ( 6.390983399715593372, 5.837459000499768180, -0.1107755759658281131 ) ) ;
#4231=( GEOMETRIC_REPRESENTATION_CONTEXT ( 3 ) GLOBAL_UNCERTAINTY_ASSIGNED_CONTEXT ( ( #595 ) ) GLOBAL_UNIT_ASSIGNED_CONTEXT ( ( #7441, #4947, #718 ) ) REPRESENTATION_CONTEXT ( 'NONE', 'WORKASPACE' ) );
#4261=AXIS2_PLACEMENT_3D ( 'NONE', #9619, #4015, #13020 ) ;
#4270=LINE ( 'NONE', #925, #7994 ) ;
#4278=CIRCLE ( 'NONE', #4762, 8.105212085995399107 ) ;
#4347=CARTESIAN_POINT ( 'NONE',  ( 0.000000000000000000, 0.000000000000000000, 0.000000000000000000 ) ) ;
#4364=CARTESIAN_POINT ( 'NONE',  ( 6.534838248920899595, -2.951765777552421532, -5.112608298763837489 ) ) ;
#4390=EDGE_CURVE ( 'NONE', #11464, #1949, #11189, .T. ) ;
#4403=CARTESIAN_POINT ( 'NONE',  ( 0.000000000000000000, 0.000000000000000000, 0.000000000000000000 ) ) ;
#4413=CARTESIAN_POINT ( 'NONE',  ( 6.445127866599366762, 5.657054305385774917, 0.4229901806197435277 ) ) ;
#4442=CARTESIAN_POINT ( 'NONE',  ( 6.212068001622697011, -3.310128279683407282, -4.266689640017786722 ) ) ;
#4475=EDGE_CURVE ( 'NONE', #2146, #14514, #12247, .T. ) ;
#4478=B_SPLINE_CURVE_WITH_KNOTS ( 'NONE', 3,
 ( #6998, #2934, #10323, #12890, #10747, #1392, #2777, #5897, #10604, #11768, #487, #3900, #1677, #6183, #5081, #9576 ),
 .UNSPECIFIED., .F., .F.,
 ( 4, 3, 3, 3, 3, 4 ),
 ( -2.669610558406018255E-06, 0.000000000000000000, 5.703179328865577653E-05, 0.0001157653700801011267, 0.0001686517580788931929, 0.0002219032271218163556 ),
 .UNSPECIFIED. ) ;
#4485=CARTESIAN_POINT ( 'NONE',  ( 0.4465819873849480870, -2.886751345948518566, -5.000000000000000000 ) ) ;
#4490=CARTESIAN_POINT ( 'NONE',  ( 6.196878017913831194, -5.292377467571574456, 0.8333333333333328152 ) ) ;
#4495=EDGE_CURVE ( 'NONE', #6201, #2146, #8810, .T. ) ;
#4512=CARTESIAN_POINT ( 'NONE',  ( 6.534533895392296898, -5.902695350657469753, 2.508608540288783656E-15 ) ) ;
#4529=CARTESIAN_POINT ( 'NONE',  ( 6.244297270353402318, 0.9889575675955702971, -5.105276777067857097 ) ) ;
#4531=SURFACE_SIDE_STYLE ('',( #133 ) ) ;
#4534=CARTESIAN_POINT ( 'NONE',  ( 6.355324643801636419, -1.972141403783273850, 5.108685331087992942 ) ) ;
#4543=EDGE_CURVE ( 'NONE', #2701, #14449, #1362, .T. ) ;
#4547=CARTESIAN_POINT ( 'NONE',  ( 6.495567275914605254, 5.834887664330116408, -1.517037228251972982E-15 ) ) ;
#4551=CARTESIAN_POINT ( 'NONE',  ( 8.500000000000000000, -2.886751345948134873, -5.000000000000000000 ) ) ;
#4553=ORIENTED_EDGE ( 'NONE', *, *, #4147, .F. ) ;
#4586=CARTESIAN_POINT ( 'NONE',  ( 6.518095160332177507, -5.866179305614763528, -5.948047347825906810E-16 ) ) ;
#4599=CARTESIAN_POINT ( 'NONE',  ( 6.506891779418575439, -2.833891091414765029, -5.091556646552820808 ) ) ;
#4630=CARTESIAN_POINT ( 'NONE',  ( 6.244297270355323448, 0.4917101305082346441, 5.105276777067912164 ) ) ;
#4636=CARTESIAN_POINT ( 'NONE',  ( 6.367873360227559232, -5.773502691896264416, 0.000000000000000000 ) ) ;
#4661=AXIS2_PLACEMENT_3D ( 'NONE', #1336, #12398, #131 ) ;
#4665=CONICAL_SURFACE ( 'NONE', #7724, 5.000000000000000888, 1.047197551196600296 ) ;
#4695=FACE_OUTER_BOUND ( 'NONE', #1984, .T. ) ;
#4697=AXIS2_PLACEMENT_3D ( 'NONE', #13351, #8791, #13217 ) ;
#4716=EDGE_LOOP ( 'NONE', ( #7226, #9896, #9589, #7453 ) ) ;
#4747=CARTESIAN_POINT ( 'NONE',  ( 6.403457969954073903, -2.888443235695458355, 5.002930439003193896 ) ) ;
#4753=CARTESIAN_POINT ( 'NONE',  ( 6.362374563308424769, -3.415000007735117027, -4.302769906043429238 ) ) ;
#4762=AXIS2_PLACEMENT_3D ( 'NONE', #12210, #8549, #1816 ) ;
#4812=CARTESIAN_POINT ( 'NONE',  ( 0.000000000000000000, -4.330127018922194537, -2.500000000000000444 ) ) ;
#4832=CARTESIAN_POINT ( 'NONE',  ( 6.207530437345011087, 3.810448612249821565, 3.400109403952575882 ) ) ;
#4837=CARTESIAN_POINT ( 'NONE',  ( 6.534838248920899595, 5.903531555104835071, -2.091255385257999292E-17 ) ) ;
#4857=CARTESIAN_POINT ( 'NONE',  ( 6.371506350351444858, -3.439339428956428080, 4.260454149911180544 ) ) ;
#4859=ORIENTED_EDGE ( 'NONE', *, *, #11310, .F. ) ;
#4870=CARTESIAN_POINT ( 'NONE',  ( 0.1983443223721602366, -5.300482436767283367, -0.8192951148925881055 ) ) ;
#4874=CARTESIAN_POINT ( 'NONE',  ( 0.1973348417602838190, -1.936114729415324920, -5.000000000000000000 ) ) ;
#4875=ORIENTED_EDGE ( 'NONE', *, *, #10891, .T. ) ;
#4884=CARTESIAN_POINT ( 'NONE',  ( 6.420058897733096792, -2.891482565094588342, 5.008194711943423805 ) ) ;
#4889=CARTESIAN_POINT ( 'NONE',  ( 0.08165819712376926054, 4.939961795957294122, 1.443735181952768620 ) ) ;
#4904=DIRECTION ( 'NONE',  ( 1.000000000000000000, 0.000000000000000000, -0.000000000000000000 ) ) ;
#4939=CARTESIAN_POINT ( 'NONE',  ( 0.4465819873852049926, -5.773502691896264416, 5.911082023588295771E-17 ) ) ;
#4945=ORIENTED_EDGE ( 'NONE', *, *, #12312, .F. ) ;
#4947=( NAMED_UNIT ( * ) PLANE_ANGLE_UNIT ( ) SI_UNIT ( $, .RADIAN. ) );
#4952=CARTESIAN_POINT ( 'NONE',  ( 6.323290364501794159, 2.010128762266915725, 4.999999999999998224 ) ) ;
#4974=ORIENTED_EDGE ( 'NONE', *, *, #4475, .T. ) ;
#4997=AXIS2_PLACEMENT_3D ( 'NONE', #7878, #10160, #12363 ) ;
#5055=EDGE_CURVE ( 'NONE', #3065, #9114, #6808, .T. ) ;
#5057=ADVANCED_FACE ( 'NONE', ( #2230 ), #14039, .F. ) ;
#5076=DIRECTION ( 'NONE',  ( -1.000000000000000000, 0.000000000000000000, -0.000000000000000000 ) ) ;
#5081=CARTESIAN_POINT ( 'NONE',  ( 6.385552186430389021, 2.886751345948121550, -5.000000000000001776 ) ) ;
#5100=CARTESIAN_POINT ( 'NONE',  ( 6.242800618755127928, 3.923709308887747937, -3.414402460853335430 ) ) ;
#5105=DIRECTION ( 'NONE',  ( -1.000000000000000000, -0.000000000000000000, -0.000000000000000000 ) ) ;
#5115=CARTESIAN_POINT ( 'NONE',  ( 0.000000000000000000, 0.000000000000000000, 0.000000000000000000 ) ) ;
#5119=FACE_OUTER_BOUND ( 'NONE', #4177, .T. ) ;
#5133=AXIS2_PLACEMENT_3D ( 'NONE', #8303, #2699, #2763 ) ;
#5186=DIRECTION ( 'NONE',  ( 0.000000000000000000, 0.000000000000000000, -1.000000000000000000 ) ) ;
#5205=AXIS2_PLACEMENT_3D ( 'NONE', #5474, #11289, #11069 ) ;
#5207=VECTOR ( 'NONE', #20, 1000.000000000000114 ) ;
#5224=VECTOR ( 'NONE', #1117, 1000.000000000000000 ) ;
#5231=B_SPLINE_CURVE_WITH_KNOTS ( 'NONE', 3,
 ( #9521, #1386, #9443, #4874, #5892, #10403 ),
 .UNSPECIFIED., .F., .F.,
 ( 4, 2, 4 ),
 ( 0.01799235506992014066, 0.01945319861728520699, 0.02091404216465027679 ),
 .UNSPECIFIED. ) ;
#5240=EDGE_CURVE ( 'NONE', #10781, #9509, #11097, .T. ) ;
#5246=ORIENTED_EDGE ( 'NONE', *, *, #12791, .F. ) ;
#5248=ORIENTED_EDGE ( 'NONE', *, *, #6239, .F. ) ;
#5275=CARTESIAN_POINT ( 'NONE',  ( 6.367873360227558344, -2.886751345948134873, -5.000000000000000000 ) ) ;
#5316=CARTESIAN_POINT ( 'NONE',  ( 6.507056315241512401, 2.833450876375911420, -5.092319121366347900 ) ) ;
#5340=VERTEX_POINT ( 'NONE', #12604 ) ;
#5345=CARTESIAN_POINT ( 'NONE',  ( -4.053687927322266270E-15, 4.207632145829744097, -2.712167343862821767 ) ) ;
#5364=CARTESIAN_POINT ( 'NONE',  ( 0.3108895250735811411, -2.416698868092464370, 4.999999999999999112 ) ) ;
#5399=B_SPLINE_CURVE_WITH_KNOTS ( 'NONE', 3,
 ( #13556, #2189, #13490, #5582, #9121 ),
 .UNSPECIFIED., .F., .F.,
 ( 4, 1, 4 ),
 ( 0.000000000000000000, 0.002886751345948123347, 0.005773502691896246694 ),
 .UNSPECIFIED. ) ;
#5435=ORIENTED_EDGE ( 'NONE', *, *, #14466, .F. ) ;
#5437=CARTESIAN_POINT ( 'NONE',  ( 8.500000000000000000, 2.886751345948122882, -5.000000000000000000 ) ) ;
#5441=ORIENTED_EDGE ( 'NONE', *, *, #11512, .T. ) ;
#5474=CARTESIAN_POINT ( 'NONE',  ( 42.80949999999999278, 0.000000000000000000, 0.000000000000000000 ) ) ;
#5477=AXIS2_PLACEMENT_3D ( 'NONE', #8035, #12608, #12537 ) ;
#5494=B_SPLINE_CURVE_WITH_KNOTS ( 'NONE', 3,
 ( #348, #13961, #4747, #4884, #5908, #1330, #3555, #9378, #9152, #8051, #3636, #428, #6870, #8261, #12772, #122 ),
 .UNSPECIFIED., .F., .F.,
 ( 4, 3, 3, 3, 3, 4 ),
 ( 0.000000000000000000, 5.303647860849928001E-05, 0.0001057093501027655180, 0.0001642058037234009067, 0.0002210073443967662933, 0.0002236769549551740374 ),
 .UNSPECIFIED. ) ;
#5495=CARTESIAN_POINT ( 'NONE',  ( 0.08165819712376794215, 3.720292241887086071, -3.556264818047238041 ) ) ;
#5519=DIRECTION ( 'NONE',  ( 1.000000000000000000, 0.000000000000000000, -0.000000000000000000 ) ) ;
#5547=CARTESIAN_POINT ( 'NONE',  ( 6.323279575528021113, -5.335162385627945980, -0.7592276814620767533 ) ) ;
#5582=CARTESIAN_POINT ( 'NONE',  ( 6.196878017913834746, 1.924500897298752289, 5.000000000000000000 ) ) ;
#5598=CIRCLE ( 'NONE', #9379, 5.000000000000000000 ) ;
#5604=CARTESIAN_POINT ( 'NONE',  ( 6.436591462021368670, -5.789018756751906025, 5.182398524903814613E-16 ) ) ;
#5619=CARTESIAN_POINT ( 'NONE',  ( 6.245824673232850621, -3.903127342723632154, -3.450227696316233494 ) ) ;
#5646=EDGE_CURVE ( 'NONE', #10297, #13338, #10454, .T. ) ;
#5678=ADVANCED_FACE ( 'NONE', ( #14452 ), #3221, .T. ) ;
#5694=CARTESIAN_POINT ( 'NONE',  ( 6.196878017913830305, 5.292377467571570016, -0.8333333333333337034 ) ) ;
#5722=DIRECTION ( 'NONE',  ( -1.000000000000000000, -0.000000000000000000, -0.000000000000000000 ) ) ;
#5750=LINE ( 'NONE', #13797, #7800 ) ;
#5755=CARTESIAN_POINT ( 'NONE',  ( 6.367873360227559232, -5.773502691896264416, 0.000000000000000000 ) ) ;
#5789=LINE ( 'NONE', #4551, #4011 ) ;
#5791=ORIENTED_EDGE ( 'NONE', *, *, #2164, .T. ) ;
#5792=CARTESIAN_POINT ( 'NONE',  ( 6.362366615495917976, 2.018765416951484593, -5.108861542006081002 ) ) ;
#5820=CARTESIAN_POINT ( 'NONE',  ( 6.390820551024316565, -3.013776919160863876, 4.999999999999999112 ) ) ;
#5850=CARTESIAN_POINT ( 'NONE',  ( 6.534533895392296010, -2.951347675328738873, -5.111884124469658452 ) ) ;
#5862=CARTESIAN_POINT ( 'NONE',  ( 6.204471256524902500, -0.9979289516705972529, -5.000000000000444089 ) ) ;
#5892=CARTESIAN_POINT ( 'NONE',  ( 0.3108895250736378735, -2.416698868092693075, -5.000000000000000000 ) ) ;
#5897=CARTESIAN_POINT ( 'NONE',  ( 6.495567275914614136, 2.917443832165055539, -5.053160945538337501 ) ) ;
#5902=CARTESIAN_POINT ( 'NONE',  ( 6.212075932873402984, -2.040040303548923628, 4.999999999999999112 ) ) ;
#5908=CARTESIAN_POINT ( 'NONE',  ( 6.436591462021373999, -2.894509378375943243, 5.013437306331755217 ) ) ;
#5918=DIRECTION ( 'NONE',  ( -1.000000000000000000, -0.000000000000000000, -0.000000000000000000 ) ) ;
#5921=CARTESIAN_POINT ( 'NONE',  ( 6.367873360227556567, 2.886751345948125547, 4.999999999999999112 ) ) ;
#5922=ORIENTED_EDGE ( 'NONE', *, *, #544, .F. ) ;
#5951=EDGE_CURVE ( 'NONE', #10586, #14514, #2489, .T. ) ;
#5954=PRODUCT_DEFINITION_FORMATION_WITH_SPECIFIED_SOURCE ( 'ANY', '', #13474, .NOT_KNOWN. ) ;
#5957=FACE_OUTER_BOUND ( 'NONE', #9825, .T. ) ;
#5958=CARTESIAN_POINT ( 'NONE',  ( 6.534838248920896930, -2.951765777552407766, 5.112608298763836601 ) ) ;
#5967=CARTESIAN_POINT ( 'NONE',  ( -4.137823196307924351E-15, 4.821944789745366222, -1.648146632869000427 ) ) ;
#5978=CARTESIAN_POINT ( 'NONE',  ( 6.095484975317565279, -1.047622383848427985, 4.999999999999999112 ) ) ;
#5979=ORIENTED_EDGE ( 'NONE', *, *, #11276, .T. ) ;
#6003=ADVANCED_FACE ( 'NONE', ( #3822 ), #12901, .T. ) ;
#6016=EDGE_LOOP ( 'NONE', ( #1276, #9249, #13479 ) ) ;
#6034=DIRECTION ( 'NONE',  ( -0.7071067811865530128, 0.000000000000000000, 0.7071067811865421326 ) ) ;
#6084=EDGE_LOOP ( 'NONE', ( #11470, #14535, #11003, #8827, #13799, #3144, #2964 ) ) ;
#6090=CARTESIAN_POINT ( 'NONE',  ( 0.000000000000000000, 0.000000000000000000, -5.000000000000000000 ) ) ;
#6097=VECTOR ( 'NONE', #5105, 1000.000000000000000 ) ;
#6102=ORIENTED_EDGE ( 'NONE', *, *, #6483, .F. ) ;
#6109=EDGE_CURVE ( 'NONE', #8256, #10297, #11522, .T. ) ;
#6118=CARTESIAN_POINT ( 'NONE',  ( 0.3106000600989253235, -3.122278952918442041, 4.592054218142292754 ) ) ;
#6131=CARTESIAN_POINT ( 'NONE',  ( 8.500000000000000000, 2.886751345948125547, 4.999999999999999112 ) ) ;
#6137=CARTESIAN_POINT ( 'NONE',  ( 0.1739375980333739413, -5.301268757141563981, 0.8179331680533016291 ) ) ;
#6143=CARTESIAN_POINT ( 'NONE',  ( 6.420058897733091463, 2.891482565094592339, 5.008194711943422028 ) ) ;
#6156=CARTESIAN_POINT ( 'NONE',  ( 6.420058897733093239, -2.891482565094601220, -5.008194711943422917 ) ) ;
#6183=CARTESIAN_POINT ( 'NONE',  ( 6.403457969954074791, 2.888443235695460576, -5.002930439003194785 ) ) ;
#6187=FACE_OUTER_BOUND ( 'NONE', #6962, .T. ) ;
#6201=VERTEX_POINT ( 'NONE', #4485 ) ;
#6239=EDGE_CURVE ( 'NONE', #8256, #3065, #5399, .T. ) ;
#6254=EDGE_LOOP ( 'NONE', ( #3603, #4974, #6351 ) ) ;
#6264=VERTEX_POINT ( 'NONE', #6838 ) ;
#6271=CARTESIAN_POINT ( 'NONE',  ( 0.01055556052338940849, 4.575665857285979854, 2.074714256722482553 ) ) ;
#6311=CARTESIAN_POINT ( 'NONE',  ( 6.507056315241511513, -2.833450876375909644, 5.092319121366348789 ) ) ;
#6330=CARTESIAN_POINT ( 'NONE',  ( 0.000000000000000000, 0.000000000000000000, 5.000000000000000888 ) ) ;
#6344=CARTESIAN_POINT ( 'NONE',  ( 6.204460410672268722, 3.831267809383453571, -3.364049496744554002 ) ) ;
#6345=EDGE_CURVE ( 'NONE', #3667, #14024, #10303, .T. ) ;
#6350=CARTESIAN_POINT ( 'NONE',  ( 42.80949999999999278, 0.000000000000000000, 0.000000000000000000 ) ) ;
#6351=ORIENTED_EDGE ( 'NONE', *, *, #935, .T. ) ;
#6352=FACE_OUTER_BOUND ( 'NONE', #11498, .T. ) ;
#6362=AXIS2_PLACEMENT_3D ( 'NONE', #10458, #5076, #478 ) ;
#6364=AXIS2_PLACEMENT_3D ( 'NONE', #895, #6597, #763 ) ;
#6393=CARTESIAN_POINT ( 'NONE',  ( 6.506891779418576327, -5.826362946429632927, -0.09155664655281940678 ) ) ;
#6417=DIRECTION ( 'NONE',  ( 1.000000000000000000, 0.000000000000000000, 0.000000000000000000 ) ) ;
#6420=CARTESIAN_POINT ( 'NONE',  ( 6.534838248920897819, 2.951765777552412651, 5.112608298763836601 ) ) ;
#6441=B_SPLINE_CURVE_WITH_KNOTS ( 'NONE', 3,
 ( #4636, #4490, #2418, #10238, #8094 ),
 .UNSPECIFIED., .F., .F.,
 ( 4, 1, 4 ),
 ( 0.000000000000000000, 0.002886751345948132021, 0.005773502691896264041 ),
 .UNSPECIFIED. ) ;
#6454=B_SPLINE_CURVE_WITH_KNOTS ( 'NONE', 3,
 ( #63, #4529, #9023, #1188 ),
 .UNSPECIFIED., .F., .F.,
 ( 4, 4 ),
 ( 0.002977824986803846545, 0.005972417098209359745 ),
 .UNSPECIFIED. ) ;
#6477=CARTESIAN_POINT ( 'NONE',  ( 0.000000000000000000, 0.000000000000000000, 0.000000000000000000 ) ) ;
#6480=CARTESIAN_POINT ( 'NONE',  ( 0.4465819873849480870, -2.886751345948518566, -5.000000000000000000 ) ) ;
#6482=CARTESIAN_POINT ( 'NONE',  ( 0.000000000000000000, 0.000000000000000000, 5.000000000000000888 ) ) ;
#6483=EDGE_CURVE ( 'NONE', #248, #14449, #2778, .T. ) ;
#6485=CARTESIAN_POINT ( 'NONE',  ( 0.000000000000000000, 5.773502691896261751, -2.749426538070115714E-16 ) ) ;
#6503=CARTESIAN_POINT ( 'NONE',  ( 6.244004651191002786, -4.663678638742300819, -2.132808149174402423 ) ) ;
#6514=DIRECTION ( 'NONE',  ( 0.000000000000000000, 0.000000000000000000, 1.000000000000000000 ) ) ;
#6525=CARTESIAN_POINT ( 'NONE',  ( 0.4465819873851997746, 2.886751345948125547, 4.999999999999999112 ) ) ;
#6530=CARTESIAN_POINT ( 'NONE',  ( 6.323279575526099983, -3.325091652216674909, 4.240772318537645802 ) ) ;
#6583=DIRECTION ( 'NONE',  ( -1.000000000000000000, -0.000000000000000000, -0.000000000000000000 ) ) ;
#6597=DIRECTION ( 'NONE',  ( 1.000000000000000000, 0.000000000000000000, 0.000000000000000000 ) ) ;
#6629=AXIS2_PLACEMENT_3D ( 'NONE', #14388, #10099, #12447 ) ;
#6650=DIRECTION ( 'NONE',  ( 0.000000000000000000, 0.000000000000000000, -1.000000000000000000 ) ) ;
#6656=AXIS2_PLACEMENT_3D ( 'NONE', #13990, #2459, #6963 ) ;
#6658=CARTESIAN_POINT ( 'NONE',  ( 6.367873360227558344, 5.773502691896261751, 0.000000000000000000 ) ) ;
#6688=DIRECTION ( 'NONE',  ( -1.000000000000000000, -0.000000000000000000, -0.000000000000000000 ) ) ;
#6725=CARTESIAN_POINT ( 'NONE',  ( 6.204460410672267834, -4.828986228461507046, -1.635950503254239408 ) ) ;
#6746=ORIENTED_EDGE ( 'NONE', *, *, #7330, .F. ) ;
#6750=CARTESIAN_POINT ( 'NONE',  ( 6.207660606242546564, -2.016205878029795784, -5.000000000000000000 ) ) ;
#6774=DIRECTION ( 'NONE',  ( -1.000000000000000000, -0.000000000000000000, -0.000000000000000000 ) ) ;
#6796=CONICAL_SURFACE ( 'NONE', #4697, 5.000000000000000888, 1.047197551196600296 ) ;
#6808=LINE ( 'NONE', #6131, #5224 ) ;
#6818=CARTESIAN_POINT ( 'NONE',  ( 6.452281807715712247, 5.797857616946122228, 9.234669952027924180E-16 ) ) ;
#6825=ORIENTED_EDGE ( 'NONE', *, *, #7196, .T. ) ;
#6838=CARTESIAN_POINT ( 'NONE',  ( 43.50000000000000711, 4.475777889183788807E-16, -3.309499999999999886 ) ) ;
#6869=CARTESIAN_POINT ( 'NONE',  ( 6.196878017913830305, 3.367876570272813730, -4.166666666666666963 ) ) ;
#6870=CARTESIAN_POINT ( 'NONE',  ( 6.533910050139692949, -2.950514251728062476, 5.110440592449057462 ) ) ;
#6876=CARTESIAN_POINT ( 'NONE',  ( 6.207530437345013752, -3.810448612250150635, -3.400109403952463971 ) ) ;
#6890=CIRCLE ( 'NONE', #521, 3.309499999999999886 ) ;
#6891=VERTEX_POINT ( 'NONE', #1790 ) ;
#6905=CARTESIAN_POINT ( 'NONE',  ( 6.541171952014627422, 2.986180817377861452, -5.112746308113085725 ) ) ;
#6923=EDGE_CURVE ( 'NONE', #14237, #11464, #73, .T. ) ;
#6945=CARTESIAN_POINT ( 'NONE',  ( 0.000000000000000000, 0.000000000000000000, 0.000000000000000000 ) ) ;
#6961=ORIENTED_EDGE ( 'NONE', *, *, #3278, .T. ) ;
#6962=EDGE_LOOP ( 'NONE', ( #3595, #13163, #10639, #4945 ) ) ;
#6963=DIRECTION ( 'NONE',  ( 0.000000000000000000, 0.000000000000000000, 1.000000000000000000 ) ) ;
#6972=CARTESIAN_POINT ( 'NONE',  ( 6.390821132688881967, 3.013780087859768919, -5.000000000000000000 ) ) ;
#6983=ORIENTED_EDGE ( 'NONE', *, *, #1765, .T. ) ;
#6998=CARTESIAN_POINT ( 'NONE',  ( 6.534838248920896930, 2.951765777552409986, -5.112608298763837489 ) ) ;
#7001=CARTESIAN_POINT ( 'NONE',  ( 6.541334450618641938, 2.987059910623325987, 5.112749838330405083 ) ) ;
#7033=CARTESIAN_POINT ( 'NONE',  ( 6.534533895392296010, 5.902695350657467088, 8.411391101939246700E-15 ) ) ;
#7050=CARTESIAN_POINT ( 'NONE',  ( 6.244889965166093404, -4.918546365148220190, 1.691415889817839968 ) ) ;
#7073=MANIFOLD_SOLID_BREP ( 'FlangeHexFillet', #14227 ) ;
#7077=EDGE_CURVE ( 'NONE', #13548, #9831, #956, .T. ) ;
#7079=CARTESIAN_POINT ( 'NONE',  ( 6.207682235858348108, 2.016324304256104760, 4.999999999999999112 ) ) ;
#7098=CARTESIAN_POINT ( 'NONE',  ( 6.534838248920897819, 2.951765777552412651, 5.112608298763836601 ) ) ;
#7154=CARTESIAN_POINT ( 'NONE',  ( 6.445379721942640749, -2.463581311471621849, -5.110653333236677476 ) ) ;
#7163=CARTESIAN_POINT ( 'NONE',  ( 6.534838248920896930, 2.951765777552409986, -5.112608298763837489 ) ) ;
#7164=EDGE_CURVE ( 'NONE', #2958, #8217, #7854, .T. ) ;
#7183=CARTESIAN_POINT ( 'NONE',  ( 6.466260427357664931, -2.904280683598016832, -5.030361703432624232 ) ) ;
#7194=EDGE_LOOP ( 'NONE', ( #616, #1743, #14282, #36 ) ) ;
#7196=EDGE_CURVE ( 'NONE', #11464, #8256, #6441, .T. ) ;
#7204=CARTESIAN_POINT ( 'NONE',  ( 6.244004651191001010, -4.178905357954648458, 2.972460101650454600 ) ) ;
#7226=ORIENTED_EDGE ( 'NONE', *, *, #13399, .F. ) ;
#7251=AXIS2_PLACEMENT_3D ( 'NONE', #13043, #7426, #8825 ) ;
#7253=CARTESIAN_POINT ( 'NONE',  ( 6.506987859255521478, -2.925375531177301980, -5.066899051217866656 ) ) ;
#7259=ORIENTED_EDGE ( 'NONE', *, *, #9910, .T. ) ;
#7330=EDGE_CURVE ( 'NONE', #9114, #9269, #14352, .T. ) ;
#7376=CARTESIAN_POINT ( 'NONE',  ( 6.371506350351443082, 3.439339428956428968, -4.260454149911181432 ) ) ;
#7392=CARTESIAN_POINT ( 'NONE',  ( 8.500000000000000000, 5.773502691896261751, 0.000000000000000000 ) ) ;
#7426=DIRECTION ( 'NONE',  ( -1.000000000000000000, -0.000000000000000000, -0.000000000000000000 ) ) ;
#7435=ORIENTED_EDGE ( 'NONE', *, *, #5055, .F. ) ;
#7441=( LENGTH_UNIT ( ) NAMED_UNIT ( * ) SI_UNIT ( .MILLI., .METRE. ) );
#7449=CARTESIAN_POINT ( 'NONE',  ( 6.357976367242160975, 3.426708043488479127, -4.282301071215555588 ) ) ;
#7453=ORIENTED_EDGE ( 'NONE', *, *, #10891, .F. ) ;
#7456=DIRECTION ( 'NONE',  ( -0.000000000000000000, 0.000000000000000000, 1.000000000000000000 ) ) ;
#7459=VERTEX_POINT ( 'NONE', #13393 ) ;
#7467=ADVANCED_FACE ( 'NONE', ( #4118 ), #8763, .F. ) ;
#7468=CARTESIAN_POINT ( 'NONE',  ( 7.336184427528458230, 0.000000000000000000, -8.105212085995399107 ) ) ;
#7479=DIRECTION ( 'NONE',  ( 0.000000000000000000, 0.5000000000000009992, -0.8660254037844380415 ) ) ;
#7520=( BOUNDED_SURFACE ( )  B_SPLINE_SURFACE ( 3, 2, ( 
 ( #219, #3650, #8129 ),
 ( #12637, #2519, #1422 ),
 ( #296, #4832, #9324 ),
 ( #3718, #8201, #10939 ),
 ( #9829, #8579, #4090 ),
 ( #4223, #14331, #10786 ) ),
 .UNSPECIFIED., .F., .F., .T. ) 
 B_SPLINE_SURFACE_WITH_KNOTS ( ( 4, 2, 4 ),
 ( 3, 3 ),
 ( 0.02367865728600889244, 0.02663179453327095547, 0.02958493178053301503 ),
 ( 0.000000000000000000, 1.000000000000000000 ),
 .UNSPECIFIED. ) 
 GEOMETRIC_REPRESENTATION_ITEM ( )  RATIONAL_B_SPLINE_SURFACE ( (
 ( 1.000000000000000000, 0.8047781103519378032, 1.000000000000000000),
 ( 1.000000000000000000, 0.8123785825977077879, 1.000000000000000000),
 ( 1.000000000000000000, 0.8190671539292031511, 1.000000000000000000),
 ( 1.000000000000000000, 0.8192352255331103450, 1.000000000000000000),
 ( 1.000000000000000000, 0.8126129676838903526, 1.000000000000000000),
 ( 1.000000000000000000, 0.8047712537969723412, 1.000000000000000000) ) ) 
 REPRESENTATION_ITEM ( '' )  SURFACE ( )  );
#7522=MECHANICAL_DESIGN_GEOMETRIC_PRESENTATION_REPRESENTATION('',(#11995),#4231);
#7565=EDGE_CURVE ( 'NONE', #14237, #6201, #5789, .T. ) ;
#7588=( GEOMETRIC_REPRESENTATION_CONTEXT ( 3 ) GLOBAL_UNCERTAINTY_ASSIGNED_CONTEXT ( ( #11939 ) ) GLOBAL_UNIT_ASSIGNED_CONTEXT ( ( #4163, #1109, #7916 ) ) REPRESENTATION_CONTEXT ( 'NONE', 'WORKASPACE' ) );
#7589=ORIENTED_EDGE ( 'NONE', *, *, #11515, .F. ) ;
#7614=CARTESIAN_POINT ( 'NONE',  ( 6.371506350351448411, -5.409331239960140536, -0.8483282427581464447 ) ) ;
#7621=ADVANCED_FACE ( 'NONE', ( #9267 ), #152, .T. ) ;
#7626=ADVANCED_FACE ( 'NONE', ( #4695 ), #3548, .T. ) ;
#7648=CARTESIAN_POINT ( 'NONE',  ( 6.327632967269667397, -5.346704644972363418, 0.7392359018475850307 ) ) ;
#7661=CARTESIAN_POINT ( 'NONE',  ( -7.882332067283284779E-16, -3.838309248099061932, -3.351853367130940509 ) ) ;
#7673=AXIS2_PLACEMENT_3D ( 'NONE', #6350, #13138, #8709 ) ;
#7724=AXIS2_PLACEMENT_3D ( 'NONE', #6945, #11442, #10338 ) ;
#7733=ADVANCED_FACE ( 'NONE', ( #2692 ), #2917, .F. ) ;
#7772=SURFACE_STYLE_USAGE ( .BOTH. , #4531 ) ;
#7775=CARTESIAN_POINT ( 'NONE',  ( 6.244297270354683960, 1.800816419761795034E-11, 5.105276777067893512 ) ) ;
#7778=ORIENTED_EDGE ( 'NONE', *, *, #4147, .T. ) ;
#7779=CARTESIAN_POINT ( 'NONE',  ( 0.05140428708382503709, 3.841181488860375470, -3.346878500200758833 ) ) ;
#7780=DIRECTION ( 'NONE',  ( 0.000000000000000000, -1.224646799147353700E-16, 1.000000000000000000 ) ) ;
#7788=CARTESIAN_POINT ( 'NONE',  ( 6.534838248920900483, -5.903531555104837736, 5.201568163584232486E-16 ) ) ;
#7789=DIRECTION ( 'NONE',  ( -1.000000000000000000, -0.000000000000000000, -0.000000000000000000 ) ) ;
#7800=VECTOR ( 'NONE', #2347, 999.9999999999998863 ) ;
#7807=CARTESIAN_POINT ( 'NONE',  ( 0.3117969352650126202, 2.419842229202155082, 4.999999999999999112 ) ) ;
#7815=ORIENTED_EDGE ( 'NONE', *, *, #11747, .T. ) ;
#7854=B_SPLINE_CURVE_WITH_KNOTS ( 'NONE', 3,
 ( #11198, #4413, #12300, #13200, #3016, #12010, #1907, #6420 ),
 .UNSPECIFIED., .F., .F.,
 ( 4, 2, 2, 4 ),
 ( 0.000000000000000000, 0.001493104274552339720, 0.002986208549104679439, 0.005972417098209361480 ),
 .UNSPECIFIED. ) ;
#7859=DIRECTION ( 'NONE',  ( -0.000000000000000000, 1.000000000000000000, 1.224646799147353207E-16 ) ) ;
#7875=CARTESIAN_POINT ( 'NONE',  ( 6.507056081706568129, -2.993351035583803110, -4.999999999999999112 ) ) ;
#7878=CARTESIAN_POINT ( 'NONE',  ( 0.000000000000000000, 0.000000000000000000, 0.000000000000000000 ) ) ;
#7879=ORIENTED_EDGE ( 'NONE', *, *, #10760, .T. ) ;
#7899=CARTESIAN_POINT ( 'NONE',  ( 6.534224484704354907, -5.901860969583196059, 7.986458555526148407E-15 ) ) ;
#7912=FACE_OUTER_BOUND ( 'NONE', #2317, .T. ) ;
#7916=( NAMED_UNIT ( * ) SI_UNIT ( $, .STERADIAN. ) SOLID_ANGLE_UNIT ( ) );
#7933=ORIENTED_EDGE ( 'NONE', *, *, #2164, .F. ) ;
#7935=PLANE ( 'NONE',  #723 ) ;
#7940=CARTESIAN_POINT ( 'NONE',  ( 6.371919382990604674, 1.972754410575519035, 5.108792907957607099 ) ) ;
#7947=ORIENTED_EDGE ( 'NONE', *, *, #11515, .T. ) ;
#7954=EDGE_CURVE ( 'NONE', #2701, #3667, #9046, .T. ) ;
#7961=CARTESIAN_POINT ( 'NONE',  ( 6.196878017913834746, -5.292377467571577121, -0.8333333333333333703 ) ) ;
#7975=CARTESIAN_POINT ( 'NONE',  ( 6.092449800118536984, -4.833012432206698072, -1.628976913805976423 ) ) ;
#7979=EDGE_CURVE ( 'NONE', #3065, #11111, #3597, .T. ) ;
#7982=VERTEX_POINT ( 'NONE', #8947 ) ;
#7994=VECTOR ( 'NONE', #13334, 1000.000000000000000 ) ;
#8025=ORIENTED_EDGE ( 'NONE', *, *, #11330, .F. ) ;
#8035=CARTESIAN_POINT ( 'NONE',  ( 7.900000000000002132, 0.000000000000000000, 7.900000000000002132 ) ) ;
#8051=CARTESIAN_POINT ( 'NONE',  ( 6.506987859255527695, -2.925375531177292210, 5.066899051217877314 ) ) ;
#8080=CARTESIAN_POINT ( 'NONE',  ( 6.207519134556300777, 1.039264565629510528, -4.999999999999555023 ) ) ;
#8094=CARTESIAN_POINT ( 'NONE',  ( 6.367873360227555679, -2.886751345948120662, 4.999999999999999112 ) ) ;
#8104=EDGE_CURVE ( 'NONE', #3065, #8217, #1814, .T. ) ;
#8112=CARTESIAN_POINT ( 'NONE',  ( 6.362382503762741948, -2.018850626433581041, 5.108861885121540602 ) ) ;
#8129=CARTESIAN_POINT ( 'NONE',  ( 6.541171661047875396, 2.934678558896536504, 5.142480235691129664 ) ) ;
#8132=CARTESIAN_POINT ( 'NONE',  ( 6.518095160332176619, -2.933089652807386649, -5.080260301816938551 ) ) ;
#8136=CARTESIAN_POINT ( 'NONE',  ( 6.481779955677546390, 5.820445026626438256, 9.200230307558180419E-16 ) ) ;
#8141=EDGE_LOOP ( 'NONE', ( #12341, #4180 ) ) ;
#8146=ORIENTED_EDGE ( 'NONE', *, *, #5951, .F. ) ;
#8175=CARTESIAN_POINT ( 'NONE',  ( 6.092439126518621073, 1.005559546149547678, 4.999999999999999112 ) ) ;
#8193=CARTESIAN_POINT ( 'NONE',  ( 6.533910050139694725, 2.950514251728050485, 5.110440592449069896 ) ) ;
#8201=CARTESIAN_POINT ( 'NONE',  ( 6.204460410672266946, 4.828986228461177532, 1.635950503255240607 ) ) ;
#8217=VERTEX_POINT ( 'NONE', #10778 ) ;
#8222=CARTESIAN_POINT ( 'NONE',  ( 7.336184427528458230, 9.926022037524705097E-16, 8.105212085995399107 ) ) ;
#8245=AXIS2_PLACEMENT_3D ( 'NONE', #4403, #14451, #13267 ) ;
#8247=CARTESIAN_POINT ( 'NONE',  ( -3.965067105215785097E-15, -4.207632145829741432, 2.712167343862823099 ) ) ;
#8254=CARTESIAN_POINT ( 'NONE',  ( 6.506891485183659896, -2.992470280394939675, 5.000000000000000000 ) ) ;
#8256=VERTEX_POINT ( 'NONE', #12103 ) ;
#8261=CARTESIAN_POINT ( 'NONE',  ( 6.534224484704351354, -2.950930484791602471, 5.111161529262889580 ) ) ;
#8271=CARTESIAN_POINT ( 'NONE',  ( 0.1983443223721576831, 5.300482436767277150, 0.8192951148925904370 ) ) ;
#8272=CARTESIAN_POINT ( 'NONE',  ( 8.500000000000000000, 2.886751345948122882, -5.000000000000000000 ) ) ;
#8279=DIRECTION ( 'NONE',  ( -1.000000000000000000, -0.000000000000000000, -0.000000000000000000 ) ) ;
#8280=DIRECTION ( 'NONE',  ( -0.000000000000000000, 0.8660254037844387076, 0.5000000000000001110 ) ) ;
#8285=EDGE_CURVE ( 'NONE', #483, #9255, #11554, .T. ) ;
#8303=CARTESIAN_POINT ( 'NONE',  ( 7.336184427528458230, 0.000000000000000000, 0.000000000000000000 ) ) ;
#8323=CARTESIAN_POINT ( 'NONE',  ( 43.50000000000000711, 0.000000000000000000, 3.309499999999999886 ) ) ;
#8340=ORIENTED_EDGE ( 'NONE', *, *, #14608, .F. ) ;
#8342=LINE ( 'NONE', #7392, #6097 ) ;
#8359=CARTESIAN_POINT ( 'NONE',  ( 6.534838248920899595, -2.951765777552421532, -5.112608298763837489 ) ) ;
#8371=B_SPLINE_CURVE_WITH_KNOTS ( 'NONE', 3,
 ( #8359, #5850, #2746, #3806, #9328, #8132, #7253, #1565, #2687, #7183, #9485, #11740, #6156, #11673, #9553, #3936 ),
 .UNSPECIFIED., .F., .F.,
 ( 4, 3, 3, 3, 3, 4 ),
 ( -2.669610558405276678E-06, 4.235164736271501695E-22, 5.703179328867178207E-05, 0.0001157653700801148554, 0.0001686517580788998878, 0.0002219032271218163014 ),
 .UNSPECIFIED. ) ;
#8382=ORIENTED_EDGE ( 'NONE', *, *, #9646, .F. ) ;
#8399=EDGE_LOOP ( 'NONE', ( #10240, #2458, #7879, #3109, #215, #5791, #10762 ) ) ;
#8456=B_SPLINE_CURVE_WITH_KNOTS ( 'NONE', 3,
 ( #2895, #353, #6271, #12701, #4889, #8271, #12922, #11812 ),
 .UNSPECIFIED., .F., .F.,
 ( 4, 2, 2, 4 ),
 ( 0.002921158011986708155, 0.003648658599403063578, 0.004376159186819419435, 0.005831160361652130281 ),
 .UNSPECIFIED. ) ;
#8463=( BOUNDED_SURFACE ( )  B_SPLINE_SURFACE ( 3, 2, ( 
 ( #10958, #6393, #13255 ),
 ( #3146, #7648, #13040 ),
 ( #13317, #8753, #3208 ),
 ( #832, #10894, #12131 ),
 ( #2015, #6530, #11910 ),
 ( #1801, #6311, #8600 ) ),
 .UNSPECIFIED., .F., .F., .T. ) 
 B_SPLINE_SURFACE_WITH_KNOTS ( ( 4, 2, 4 ),
 ( 3, 3 ),
 ( 0.02367865728600888550, 0.02663179453327094853, 0.02958493178053300809 ),
 ( 0.000000000000000000, 1.000000000000000000 ),
 .UNSPECIFIED. ) 
 GEOMETRIC_REPRESENTATION_ITEM ( )  RATIONAL_B_SPLINE_SURFACE ( (
 ( 1.000000000000000000, 0.8047781103519400236, 1.000000000000000000),
 ( 1.000000000000000000, 0.8123785825980049946, 1.000000000000000000),
 ( 1.000000000000000000, 0.8190671539288042480, 1.000000000000000000),
 ( 1.000000000000000000, 0.8192352255335092481, 1.000000000000000000),
 ( 1.000000000000000000, 0.8126129676835895932, 1.000000000000000000),
 ( 1.000000000000000000, 0.8047712537969730073, 1.000000000000000000) ) ) 
 REPRESENTATION_ITEM ( '' )  SURFACE ( )  );
#8480=AXIS2_PLACEMENT_3D ( 'NONE', #1793, #10800, #7479 ) ;
#8546=ADVANCED_FACE ( 'NONE', ( #3770 ), #9686, .F. ) ;
#8549=DIRECTION ( 'NONE',  ( -1.000000000000000000, -0.000000000000000000, -0.000000000000000000 ) ) ;
#8565=CARTESIAN_POINT ( 'NONE',  ( 6.323279575526313145, 3.325091652215454108, -4.240772318536886409 ) ) ;
#8567=B_SPLINE_CURVE_WITH_KNOTS ( 'NONE', 3,
 ( #2391, #2302, #9330, #3656, #11535, #6818, #303, #8136, #4547, #1209, #10220, #12642, #9181, #2530, #7033, #4837 ),
 .UNSPECIFIED., .F., .F.,
 ( 4, 3, 3, 3, 3, 4 ),
 ( 0.000000000000000000, 5.303647860849277479E-05, 0.0001057093501027509761, 0.0001642058037233847250, 0.0002210073443967694375, 0.0002236769549551750945 ),
 .UNSPECIFIED. ) ;
#8579=CARTESIAN_POINT ( 'NONE',  ( 6.323279575526388641, 5.335162385629701909, 0.7592276814629709270 ) ) ;
#8600=CARTESIAN_POINT ( 'NONE',  ( 6.541334219041336162, -2.934241909852036034, 5.143243597038031467 ) ) ;
#8603=DIRECTION ( 'NONE',  ( -1.000000000000000000, -0.000000000000000000, -0.000000000000000000 ) ) ;
#8630=CARTESIAN_POINT ( 'NONE',  ( 6.092449800118089343, 3.827241605637790034, -3.371023086193853047 ) ) ;
#8667=ADVANCED_FACE ( 'NONE', ( #14448 ), #14174, .T. ) ;
#8707=B_SPLINE_CURVE_WITH_KNOTS ( 'NONE', 3,
 ( #4216, #13218, #7614, #1992, #6503, #10991, #9007, #4364 ),
 .UNSPECIFIED., .F., .F.,
 ( 4, 2, 2, 4 ),
 ( 8.442967473282902092E-20, 0.001493104274552340370, 0.002986208549104680740, 0.005972417098209361480 ),
 .UNSPECIFIED. ) ;
#8709=DIRECTION ( 'NONE',  ( 0.000000000000000000, 0.000000000000000000, 1.000000000000000000 ) ) ;
#8729=ADVANCED_FACE ( 'NONE', ( #841 ), #7935, .F. ) ;
#8753=CARTESIAN_POINT ( 'NONE',  ( 6.207530437345012864, -4.849805425594809094, 1.599890596046773972 ) ) ;
#8763=PLANE ( 'NONE',  #13900 ) ;
#8791=DIRECTION ( 'NONE',  ( 1.000000000000000000, 0.000000000000000000, 0.000000000000000000 ) ) ;
#8801=ADVANCED_FACE ( 'NONE', ( #11542 ), #11188, .F. ) ;
#8810=B_SPLINE_CURVE_WITH_KNOTS ( 'NONE', 3,
 ( #6480, #14583, #7661, #13483 ),
 .UNSPECIFIED., .F., .F.,
 ( 4, 4 ),
 ( 2.380735203086576123E-07, 0.002921158011986709890 ),
 .UNSPECIFIED. ) ;
#8825=DIRECTION ( 'NONE',  ( 0.000000000000000000, 0.000000000000000000, 1.000000000000000000 ) ) ;
#8827=ORIENTED_EDGE ( 'NONE', *, *, #12968, .T. ) ;
#8834=ORIENTED_EDGE ( 'NONE', *, *, #7565, .T. ) ;
#8840=CARTESIAN_POINT ( 'NONE',  ( 43.50000000000000711, 0.000000000000000000, 0.000000000000000000 ) ) ;
#8857=CARTESIAN_POINT ( 'NONE',  ( 6.506987859255522366, -5.850751062354595078, -3.430629538771514681E-16 ) ) ;
#8941=CARTESIAN_POINT ( 'NONE',  ( 0.000000000000000000, 0.000000000000000000, 0.000000000000000000 ) ) ;
#8947=CARTESIAN_POINT ( 'NONE',  ( 0.4465819873852032162, 5.773502691896260863, 3.074436065535979155E-16 ) ) ;
#8963=CARTESIAN_POINT ( 'NONE',  ( 7.900000000000002132, 0.000000000000000000, 0.000000000000000000 ) ) ;
#9007=CARTESIAN_POINT ( 'NONE',  ( 6.355827204229364646, -3.436818823786764732, -4.264647808192652434 ) ) ;
#9014=CIRCLE ( 'NONE', #6656, 3.309499999999999886 ) ;
#9015=CARTESIAN_POINT ( 'NONE',  ( 5.991014884144047592, 4.330127018922190096, -2.500000000000003997 ) ) ;
#9016=EDGE_CURVE ( 'NONE', #7459, #10586, #2175, .T. ) ;
#9020=VECTOR ( 'NONE', #8603, 1000.000000000000000 ) ;
#9023=CARTESIAN_POINT ( 'NONE',  ( 6.355324643801637308, 1.972141403783279623, -5.108685331087993831 ) ) ;
#9025=( NAMED_UNIT ( * ) PLANE_ANGLE_UNIT ( ) SI_UNIT ( $, .RADIAN. ) );
#9046=B_SPLINE_CURVE_WITH_KNOTS ( 'NONE', 3,
 ( #7775, #9165, #4534, #11165 ),
 .UNSPECIFIED., .F., .F.,
 ( 4, 4 ),
 ( 0.002977824986803825295, 0.005972417098209346735 ),
 .UNSPECIFIED. ) ;
#9083=ADVANCED_FACE ( 'NONE', ( #10803 ), #1173, .T. ) ;
#9084=FACE_OUTER_BOUND ( 'NONE', #9223, .T. ) ;
#9088=CARTESIAN_POINT ( 'NONE',  ( 6.390820841722130830, -2.823237767533158138, -5.110008744785250023 ) ) ;
#9114=VERTEX_POINT ( 'NONE', #6525 ) ;
#9121=CARTESIAN_POINT ( 'NONE',  ( 6.367873360227556567, 2.886751345948125547, 4.999999999999999112 ) ) ;
#9142=CARTESIAN_POINT ( 'NONE',  ( 8.500000000000000000, 0.000000000000000000, 7.900000000000002132 ) ) ;
#9148=ORIENTED_EDGE ( 'NONE', *, *, #6109, .T. ) ;
#9152=CARTESIAN_POINT ( 'NONE',  ( 6.495567275914613248, -2.917443832165054207, 5.053160945538335724 ) ) ;
#9165=CARTESIAN_POINT ( 'NONE',  ( 6.244297270353400542, -0.9889575675955623035, 5.105276777067856209 ) ) ;
#9167=ORIENTED_EDGE ( 'NONE', *, *, #4495, .F. ) ;
#9169=CARTESIAN_POINT ( 'NONE',  ( 0.000000000000000000, 4.330127018922191873, 2.500000000000005773 ) ) ;
#9180=AXIS2_PLACEMENT_3D ( 'NONE', #5115, #1781, #5186 ) ;
#9181=CARTESIAN_POINT ( 'NONE',  ( 6.533910050139697390, 5.901028503456122287, 2.527553615284464624E-14 ) ) ;
#9185=DIRECTION ( 'NONE',  ( 1.000000000000000000, 0.000000000000000000, 0.000000000000000000 ) ) ;
#9187=EDGE_LOOP ( 'NONE', ( #3388, #11185, #3928, #3662 ) ) ;
#9199=DIRECTION ( 'NONE',  ( 0.000000000000000000, 0.000000000000000000, -1.000000000000000000 ) ) ;
#9207=TOROIDAL_SURFACE ( 'NONE', #2613, 7.900000000000002132, 0.5999999999999976463 ) ;
#9209=ORIENTED_EDGE ( 'NONE', *, *, #1952, .F. ) ;
#9220=CARTESIAN_POINT ( 'NONE',  ( 0.000000000000000000, 0.000000000000000000, -5.000000000000000000 ) ) ;
#9223=EDGE_LOOP ( 'NONE', ( #5435, #7815, #2112, #10647 ) ) ;
#9248=ORIENTED_EDGE ( 'NONE', *, *, #10795, .F. ) ;
#9249=ORIENTED_EDGE ( 'NONE', *, *, #13062, .T. ) ;
#9255=VERTEX_POINT ( 'NONE', #10131 ) ;
#9256=AXIS2_PLACEMENT_3D ( 'NONE', #8941, #1103, #12471 ) ;
#9267=FACE_OUTER_BOUND ( 'NONE', #4716, .T. ) ;
#9269=VERTEX_POINT ( 'NONE', #9169 ) ;
#9298=CARTESIAN_POINT ( 'NONE',  ( 6.367873360227559232, -5.773502691896264416, 0.000000000000000000 ) ) ;
#9324=CARTESIAN_POINT ( 'NONE',  ( 6.245824673232988289, 3.903127342724162840, 3.450227696316072734 ) ) ;
#9328=CARTESIAN_POINT ( 'NONE',  ( 6.527192678185238961, -2.941622124011228578, -5.095038975456188446 ) ) ;
#9330=CARTESIAN_POINT ( 'NONE',  ( 6.403457969954072126, 5.776886471390936251, -3.630823777237011237E-16 ) ) ;
#9337=SHAPE_REPRESENTATION ( 'hex flange bolt small_iso_ISO 4162 - M8 x 35 x 22-N', ( #9440 ), #7588 ) ;
#9355=ADVANCED_FACE ( 'NONE', ( #13820 ), #10650, .F. ) ;
#9378=CARTESIAN_POINT ( 'NONE',  ( 6.481779955677554383, -2.910222513313215131, 5.040653254389295235 ) ) ;
#9379=AXIS2_PLACEMENT_3D ( 'NONE', #2592, #12999, #2669 ) ;
#9382=ORIENTED_EDGE ( 'NONE', *, *, #1952, .T. ) ;
#9436=ORIENTED_EDGE ( 'NONE', *, *, #7979, .T. ) ;
#9440=AXIS2_PLACEMENT_3D ( 'NONE', #4347, #14302, #6417 ) ;
#9443=CARTESIAN_POINT ( 'NONE',  ( 0.04201760816084220557, -0.9730571234389052693, -5.000000000000000888 ) ) ;
#9458=AXIS2_PLACEMENT_3D ( 'NONE', #963, #6583, #6514 ) ;
#9478=FACE_OUTER_BOUND ( 'NONE', #2006, .T. ) ;
#9483=AXIS2_PLACEMENT_3D ( 'NONE', #11339, #3441, #9199 ) ;
#9485=CARTESIAN_POINT ( 'NONE',  ( 6.452281807715712247, -2.898928808473065999, -5.021091983800445746 ) ) ;
#9509=VERTEX_POINT ( 'NONE', #14263 ) ;
#9521=CARTESIAN_POINT ( 'NONE',  ( 0.000000000000000000, 0.000000000000000000, -5.000000000000000000 ) ) ;
#9553=CARTESIAN_POINT ( 'NONE',  ( 6.385552186430389021, -2.886751345948134873, -5.000000000000000000 ) ) ;
#9576=CARTESIAN_POINT ( 'NONE',  ( 6.367873360227556567, 2.886751345948122882, -5.000000000000000000 ) ) ;
#9589=ORIENTED_EDGE ( 'NONE', *, *, #12069, .T. ) ;
#9609=CARTESIAN_POINT ( 'NONE',  ( 8.500000000000000000, -2.886751345948134873, -5.000000000000000000 ) ) ;
#9619=CARTESIAN_POINT ( 'NONE',  ( 0.000000000000000000, 0.000000000000000000, 0.000000000000000000 ) ) ;
#9645=ORIENTED_EDGE ( 'NONE', *, *, #7954, .F. ) ;
#9646=EDGE_CURVE ( 'NONE', #11111, #12984, #2520, .T. ) ;
#9686=( BOUNDED_SURFACE ( )  B_SPLINE_SURFACE ( 3, 2, ( 
 ( #5820, #8254, #13804 ),
 ( #5902, #195, #8112 ),
 ( #5978, #341, #13737 ),
 ( #8175, #2659, #2577 ),
 ( #7079, #4952, #11580 ),
 ( #11433, #2499, #7001 ) ),
 .UNSPECIFIED., .F., .F., .T. ) 
 B_SPLINE_SURFACE_WITH_KNOTS ( ( 4, 2, 4 ),
 ( 3, 3 ),
 ( 0.02367497856332483747, 0.02662799652435013376, 0.02958101448537543005 ),
 ( 0.000000000000000000, 1.000000000000000000 ),
 .UNSPECIFIED. ) 
 GEOMETRIC_REPRESENTATION_ITEM ( )  RATIONAL_B_SPLINE_SURFACE ( (
 ( 1.000000000000000000, 0.8047781226141854649, 1.000000000000000000),
 ( 1.000000000000000000, 0.8123782257049820821, 1.000000000000000000),
 ( 1.000000000000000000, 0.8190665358012705344, 1.000000000000000000),
 ( 1.000000000000000000, 0.8192358187342196896, 1.000000000000000000),
 ( 1.000000000000000000, 0.8126132506074239537, 1.000000000000000000),
 ( 1.000000000000000000, 0.8047712440299316095, 1.000000000000000000) ) ) 
 REPRESENTATION_ITEM ( '' )  SURFACE ( )  );
#9776=ORIENTED_EDGE ( 'NONE', *, *, #935, .F. ) ;
#9798=PLANE ( 'NONE',  #10881 ) ;
#9819=DIRECTION ( 'NONE',  ( 1.000000000000000000, 0.000000000000000000, 0.000000000000000000 ) ) ;
#9825=EDGE_LOOP ( 'NONE', ( #8025, #10564 ) ) ;
#9829=CARTESIAN_POINT ( 'NONE',  ( 6.207671477328661425, 5.338259717474330479, 0.7538629453361838095 ) ) ;
#9831=VERTEX_POINT ( 'NONE', #14482 ) ;
#9844=CARTESIAN_POINT ( 'NONE',  ( 0.000000000000000000, 4.330127018922190985, -2.500000000000007105 ) ) ;
#9866=CONICAL_SURFACE ( 'NONE', #4661, 3.309499999999999886, 0.7853981633974407295 ) ;
#9896=ORIENTED_EDGE ( 'NONE', *, *, #8285, .T. ) ;
#9910=EDGE_CURVE ( 'NONE', #13338, #9269, #13690, .T. ) ;
#9916=EDGE_LOOP ( 'NONE', ( #83, #12727, #13327, #4094, #9167 ) ) ;
#9933=DIRECTION ( 'NONE',  ( 0.000000000000000000, 0.000000000000000000, 1.000000000000000000 ) ) ;
#9943=ORIENTED_EDGE ( 'NONE', *, *, #7979, .F. ) ;
#9970=CARTESIAN_POINT ( 'NONE',  ( 6.385552186430389909, -5.773502691896264416, 3.657698248296050164E-17 ) ) ;
#10025=CARTESIAN_POINT ( 'NONE',  ( 0.4465819873851989974, -2.886751345948121106, 4.999999999999999112 ) ) ;
#10048=CARTESIAN_POINT ( 'NONE',  ( 6.196878017913830305, 3.367876570272813730, 4.166666666666666075 ) ) ;
#10073=EDGE_LOOP ( 'NONE', ( #7435, #9436, #6983, #1408, #6746 ) ) ;
#10076=DIRECTION ( 'NONE',  ( -1.000000000000000000, -0.000000000000000000, -0.000000000000000000 ) ) ;
#10099=DIRECTION ( 'NONE',  ( -1.000000000000000000, -0.000000000000000000, 0.000000000000000000 ) ) ;
#10119=CARTESIAN_POINT ( 'NONE',  ( 6.390983399715594260, -5.837459000499770845, 0.1107755759658283073 ) ) ;
#10131=CARTESIAN_POINT ( 'NONE',  ( 42.80949999999999278, 0.000000000000000000, 4.000000000000000000 ) ) ;
#10140=DIRECTION ( 'NONE',  ( -0.000000000000000000, 0.000000000000000000, -1.000000000000000000 ) ) ;
#10160=DIRECTION ( 'NONE',  ( -1.000000000000000000, -0.000000000000000000, -0.000000000000000000 ) ) ;
#10162=CARTESIAN_POINT ( 'NONE',  ( 6.445379721942638973, 2.463581311471615187, 5.110653333236676588 ) ) ;
#10173=EDGE_LOOP ( 'NONE', ( #4183, #9209, #436, #2966, #1738 ) ) ;
#10202=CARTESIAN_POINT ( 'NONE',  ( 6.095473853218073224, -3.806361898857677506, -3.407187799184166366 ) ) ;
#10208=CARTESIAN_POINT ( 'NONE',  ( 6.196878017913833858, 5.292377467571573568, 0.8333333333333322601 ) ) ;
#10220=CARTESIAN_POINT ( 'NONE',  ( 6.518095160332176619, 5.866179305614760864, -3.428454095615614408E-15 ) ) ;
#10226=ORIENTED_EDGE ( 'NONE', *, *, #13062, .F. ) ;
#10238=CARTESIAN_POINT ( 'NONE',  ( 6.196878017913830305, -3.367876570272812398, 4.166666666666666963 ) ) ;
#10240=ORIENTED_EDGE ( 'NONE', *, *, #10795, .T. ) ;
#10297=VERTEX_POINT ( 'NONE', #10025 ) ;
#10303=B_SPLINE_CURVE_WITH_KNOTS ( 'NONE', 3,
 ( #5958, #2704, #4857, #13932, #7204, #7050, #2771, #3827 ),
 .UNSPECIFIED., .F., .F.,
 ( 4, 2, 2, 4 ),
 ( 0.000000000000000000, 0.001493104274552341888, 0.002986208549104682908, 0.005972417098209365817 ),
 .UNSPECIFIED. ) ;
#10323=CARTESIAN_POINT ( 'NONE',  ( 6.534224484704352243, 2.950930484791558950, -5.111161529262918890 ) ) ;
#10338=DIRECTION ( 'NONE',  ( 0.000000000000000000, 0.000000000000000000, -1.000000000000000000 ) ) ;
#10346=ORIENTED_EDGE ( 'NONE', *, *, #5951, .T. ) ;
#10403=CARTESIAN_POINT ( 'NONE',  ( 0.4465819873849480870, -2.886751345948518566, -5.000000000000000000 ) ) ;
#10425=CARTESIAN_POINT ( 'NONE',  ( 6.436591462021366006, 2.894509378375946351, 5.013437306331752552 ) ) ;
#10454=B_SPLINE_CURVE_WITH_KNOTS ( 'NONE', 3,
 ( #13401, #5364, #1972, #3297, #3161, #6482 ),
 .UNSPECIFIED., .F., .F.,
 ( 4, 2, 4 ),
 ( 0.005339748439308727480, 0.006800846765732537422, 0.008261945092156346496 ),
 .UNSPECIFIED. ) ;
#10458=CARTESIAN_POINT ( 'NONE',  ( 43.50000000000000711, 0.000000000000000000, 0.000000000000000000 ) ) ;
#10491=ORIENTED_EDGE ( 'NONE', *, *, #5646, .F. ) ;
#10524=CARTESIAN_POINT ( 'NONE',  ( 0.000000000000000000, 4.330127018922191873, 2.500000000000005773 ) ) ;
#10555=CARTESIAN_POINT ( 'NONE',  ( -3.886530401411042201E-15, -4.821944789745366222, 1.648146632869001538 ) ) ;
#10558=TOROIDAL_SURFACE ( 'NONE', #14576, 7.900000000000002132, 0.5999999999999976463 ) ;
#10564=ORIENTED_EDGE ( 'NONE', *, *, #11747, .F. ) ;
#10586=VERTEX_POINT ( 'NONE', #12674 ) ;
#10590=CARTESIAN_POINT ( 'NONE',  ( 0.1996310553826625145, 1.947030205581108619, -5.000000000000000888 ) ) ;
#10604=CARTESIAN_POINT ( 'NONE',  ( 6.481779955677555272, 2.910222513313217352, -5.040653254389295235 ) ) ;
#10616=EDGE_CURVE ( 'NONE', #2146, #1949, #22, .T. ) ;
#10639=ORIENTED_EDGE ( 'NONE', *, *, #591, .F. ) ;
#10641=FACE_OUTER_BOUND ( 'NONE', #1715, .T. ) ;
#10647=ORIENTED_EDGE ( 'NONE', *, *, #8285, .F. ) ;
#10650=PLANE ( 'NONE',  #12763 ) ;
#10657=DIRECTION ( 'NONE',  ( -1.000000000000000000, -0.000000000000000000, -0.000000000000000000 ) ) ;
#10697=CARTESIAN_POINT ( 'NONE',  ( 6.534838248920896930, 2.951765777552409986, -5.112608298763837489 ) ) ;
#10704=CARTESIAN_POINT ( 'NONE',  ( 6.390983399715590707, 2.822795037344616453, -5.110775575965826434 ) ) ;
#10747=CARTESIAN_POINT ( 'NONE',  ( 6.527192678185238073, 2.941622124011387562, -5.095038975456095187 ) ) ;
#10757=ADVANCED_FACE ( 'NONE', ( #4056 ), #9798, .F. ) ;
#10760=EDGE_CURVE ( 'NONE', #14449, #248, #4278, .T. ) ;
#10762=ORIENTED_EDGE ( 'NONE', *, *, #7164, .T. ) ;
#10772=EDGE_CURVE ( 'NONE', #13338, #9114, #12411, .T. ) ;
#10778=CARTESIAN_POINT ( 'NONE',  ( 6.534838248920897819, 2.951765777552412651, 5.112608298763836601 ) ) ;
#10780=EDGE_LOOP ( 'NONE', ( #13571, #9645, #9248, #1035, #5248 ) ) ;
#10781=VERTEX_POINT ( 'NONE', #12516 ) ;
#10786=CARTESIAN_POINT ( 'NONE',  ( 6.541334219041338827, 5.921300567812616933, -0.03049376373817709943 ) ) ;
#10795=EDGE_CURVE ( 'NONE', #8217, #2701, #621, .T. ) ;
#10800=DIRECTION ( 'NONE',  ( 0.000000000000000000, -0.8660254037844380415, -0.5000000000000009992 ) ) ;
#10803=FACE_OUTER_BOUND ( 'NONE', #8399, .T. ) ;
#10881=AXIS2_PLACEMENT_3D ( 'NONE', #6485, #5519, #13333 ) ;
#10891=EDGE_CURVE ( 'NONE', #9509, #10781, #12528, .T. ) ;
#10893=ORIENTED_EDGE ( 'NONE', *, *, #5055, .T. ) ;
#10894=CARTESIAN_POINT ( 'NONE',  ( 6.204460410672268722, -3.831267809383453571, 3.364049496744554002 ) ) ;
#10926=B_SPLINE_CURVE_WITH_KNOTS ( 'NONE', 3,
 ( #10697, #12764, #7376, #12985, #11869, #1540, #272, #13867 ),
 .UNSPECIFIED., .F., .F.,
 ( 4, 2, 2, 4 ),
 ( 0.000000000000000000, 0.001493104274552342322, 0.002986208549104683342, 0.005972417098209364950 ),
 .UNSPECIFIED. ) ;
#10939=CARTESIAN_POINT ( 'NONE',  ( 6.242800618755108388, 4.918813924286816963, 1.690830708135752758 ) ) ;
#10958=CARTESIAN_POINT ( 'NONE',  ( 6.390820841722131718, -5.837016270311241151, -0.1100087447852492878 ) ) ;
#10991=CARTESIAN_POINT ( 'NONE',  ( 6.244889965166096069, -3.924082311521026600, -3.413878157001048574 ) ) ;
#11003=ORIENTED_EDGE ( 'NONE', *, *, #6345, .T. ) ;
#11024=CARTESIAN_POINT ( 'NONE',  ( 6.367873360227558344, 5.773502691896261751, 0.000000000000000000 ) ) ;
#11051=AXIS2_PLACEMENT_3D ( 'NONE', #2811, #7456, #9819 ) ;
#11069=DIRECTION ( 'NONE',  ( 0.000000000000000000, 0.000000000000000000, 1.000000000000000000 ) ) ;
#11094=CARTESIAN_POINT ( 'NONE',  ( 0.1983443223721556292, 3.359771601077104375, -4.180704885107414448 ) ) ;
#11097=CIRCLE ( 'NONE', #6629, 4.000000000000000000 ) ;
#11101=ADVANCED_FACE ( 'NONE', ( #4112 ), #8463, .F. ) ;
#11102=ORIENTED_EDGE ( 'NONE', *, *, #12968, .F. ) ;
#11111=VERTEX_POINT ( 'NONE', #11024 ) ;
#11164=PRESENTATION_STYLE_ASSIGNMENT (( #7772 ) ) ;
#11165=CARTESIAN_POINT ( 'NONE',  ( 6.534838248920896930, -2.951765777552407766, 5.112608298763836601 ) ) ;
#11177=FACE_BOUND ( 'NONE', #13778, .T. ) ;
#11185=ORIENTED_EDGE ( 'NONE', *, *, #7196, .F. ) ;
#11186=DIRECTION ( 'NONE',  ( 1.000000000000000000, 0.000000000000000000, 0.000000000000000000 ) ) ;
#11188=( BOUNDED_SURFACE ( )  B_SPLINE_SURFACE ( 3, 2, ( 
 ( #6972, #11466, #6905 ),
 ( #17, #11404, #5792 ),
 ( #1443, #8080, #13698 ),
 ( #1359, #5862, #2243 ),
 ( #6750, #1137, #11329 ),
 ( #1219, #7875, #3664 ) ),
 .UNSPECIFIED., .F., .F., .F. ) 
 B_SPLINE_SURFACE_WITH_KNOTS ( ( 4, 2, 4 ),
 ( 3, 3 ),
 ( 0.02368235114939812661, 0.02663560780161266378, 0.02958886445382720443 ),
 ( 0.000000000000000000, 1.000000000000000000 ),
 .UNSPECIFIED. ) 
 GEOMETRIC_REPRESENTATION_ITEM ( )  RATIONAL_B_SPLINE_SURFACE ( (
 ( 1.000000000000000000, 0.8047780980783512117, 1.000000000000000000),
 ( 1.000000000000000000, 0.8123789398383448601, 1.000000000000000000),
 ( 1.000000000000000000, 0.8190677725692530053, 1.000000000000000000),
 ( 1.000000000000000000, 0.8192346316605858547, 1.000000000000000000),
 ( 1.000000000000000000, 0.8126126875065294852, 1.000000000000000000),
 ( 1.000000000000000000, 0.8047712635281869531, 1.000000000000000000) ) ) 
 REPRESENTATION_ITEM ( '' )  SURFACE ( )  );
#11189=LINE ( 'NONE', #12205, #2343 ) ;
#11192=CARTESIAN_POINT ( 'NONE',  ( 6.534838248920897819, 2.951765777552412651, 5.112608298763836601 ) ) ;
#11198=CARTESIAN_POINT ( 'NONE',  ( 6.534838248920899595, 5.903531555104835071, -2.091255385257999292E-17 ) ) ;
#11205=ADVANCED_FACE ( 'NONE', ( #11177, #1283 ), #13605, .T. ) ;
#11211=ORIENTED_EDGE ( 'NONE', *, *, #11276, .F. ) ;
#11231=CARTESIAN_POINT ( 'NONE',  ( 5.991014884144048480, 4.330127018922193649, 2.500000000000001776 ) ) ;
#11236=CARTESIAN_POINT ( 'NONE',  ( 6.390820841722131718, 5.837016270311240262, 0.1100087447852529932 ) ) ;
#11243=FACE_OUTER_BOUND ( 'NONE', #1442, .T. ) ;
#11252=CARTESIAN_POINT ( 'NONE',  ( 8.500000000000000000, -5.773502691896264416, 0.000000000000000000 ) ) ;
#11271=CARTESIAN_POINT ( 'NONE',  ( 6.534838248920899595, 5.903531555104835071, -2.091255385257999292E-17 ) ) ;
#11276=EDGE_CURVE ( 'NONE', #7459, #9269, #2644, .T. ) ;
#11283=CIRCLE ( 'NONE', #2805, 0.5999999999999980904 ) ;
#11289=DIRECTION ( 'NONE',  ( -1.000000000000000000, -0.000000000000000000, -0.000000000000000000 ) ) ;
#11298=CARTESIAN_POINT ( 'NONE',  ( 6.357976367241882976, -5.421935536069461214, -0.8264656814054126555 ) ) ;
#11310=EDGE_CURVE ( 'NONE', #13548, #14237, #8371, .T. ) ;
#11314=CARTESIAN_POINT ( 'NONE',  ( 6.506891779418575439, 5.826362946429633816, 0.09155664655282295950 ) ) ;
#11329=CARTESIAN_POINT ( 'NONE',  ( 6.357965579934231393, -1.995168835100903593, -5.108766517442098198 ) ) ;
#11330=EDGE_CURVE ( 'NONE', #6891, #6264, #9014, .T. ) ;
#11339=CARTESIAN_POINT ( 'NONE',  ( 8.500000000000000000, 0.000000000000000000, 0.000000000000000000 ) ) ;
#11352=STYLED_ITEM ( 'NONE', ( #11164 ), #4067 ) ;
#11367=CARTESIAN_POINT ( 'NONE',  ( 6.466260427357666707, -5.808561367196026559, 2.605448573279809935E-16 ) ) ;
#11374=AXIS2_PLACEMENT_3D ( 'NONE', #12716, #10657, #11608 ) ;
#11378=CARTESIAN_POINT ( 'NONE',  ( 6.327632967270661268, -3.313549392876192545, -4.260764098153476453 ) ) ;
#11382=( NAMED_UNIT ( * ) SI_UNIT ( $, .STERADIAN. ) SOLID_ANGLE_UNIT ( ) );
#11404=CARTESIAN_POINT ( 'NONE',  ( 6.327625087026977013, 2.033113452596824633, -5.000000000000000000 ) ) ;
#11424=CARTESIAN_POINT ( 'NONE',  ( 7.900000000000002132, 0.000000000000000000, 0.000000000000000000 ) ) ;
#11433=CARTESIAN_POINT ( 'NONE',  ( 6.390983631292895595, 3.014665224428354495, 4.999999999999999112 ) ) ;
#11442=DIRECTION ( 'NONE',  ( 1.000000000000000000, 0.000000000000000000, 0.000000000000000000 ) ) ;
#11464=VERTEX_POINT ( 'NONE', #12449 ) ;
#11466=CARTESIAN_POINT ( 'NONE',  ( 6.506892073925697240, 2.992473431090949543, -5.000000000000000000 ) ) ;
#11470=ORIENTED_EDGE ( 'NONE', *, *, #4543, .F. ) ;
#11472=PLANE ( 'NONE',  #6362 ) ;
#11498=EDGE_LOOP ( 'NONE', ( #2926, #573, #11614 ) ) ;
#11512=EDGE_CURVE ( 'NONE', #2328, #2067, #3359, .T. ) ;
#11515=EDGE_CURVE ( 'NONE', #2067, #14449, #13724, .T. ) ;
#11522=LINE ( 'NONE', #3797, #632 ) ;
#11535=CARTESIAN_POINT ( 'NONE',  ( 6.436591462021367782, 5.789018756751902473, -4.392644635849238026E-16 ) ) ;
#11542=FACE_OUTER_BOUND ( 'NONE', #10173, .T. ) ;
#11543=AXIS2_PLACEMENT_3D ( 'NONE', #3504, #9185, #2466 ) ;
#11554=CIRCLE ( 'NONE', #5205, 4.000000000000000000 ) ;
#11565=CARTESIAN_POINT ( 'NONE',  ( 0.4465819873852032162, 5.773502691896260863, 3.074436065535979155E-16 ) ) ;
#11570=CARTESIAN_POINT ( 'NONE',  ( 0.05140428708382898532, -4.819072548984010496, -1.653121499799247163 ) ) ;
#11580=CARTESIAN_POINT ( 'NONE',  ( 6.357987042335823347, 1.995285544161284896, 5.108766985363216051 ) ) ;
#11585=AXIS2_PLACEMENT_3D ( 'NONE', #3277, #13384, #10140 ) ;
#11608=DIRECTION ( 'NONE',  ( 0.000000000000000000, 0.000000000000000000, 1.000000000000000000 ) ) ;
#11614=ORIENTED_EDGE ( 'NONE', *, *, #9910, .F. ) ;
#11639=CARTESIAN_POINT ( 'NONE',  ( 0.3106000600989304861, -5.537975084925944813, -0.4079457818577078010 ) ) ;
#11670=FACE_OUTER_BOUND ( 'NONE', #6016, .T. ) ;
#11673=CARTESIAN_POINT ( 'NONE',  ( 6.403457969954072126, -2.888443235695472122, -5.002930439003193896 ) ) ;
#11728=CARTESIAN_POINT ( 'NONE',  ( 6.403457969954070350, 2.888443235695463240, 5.002930439003193008 ) ) ;
#11740=CARTESIAN_POINT ( 'NONE',  ( 6.436591462021367782, -2.894509378375955677, -5.013437306331753440 ) ) ;
#11747=EDGE_CURVE ( 'NONE', #6264, #6891, #6890, .T. ) ;
#11768=CARTESIAN_POINT ( 'NONE',  ( 6.466260427357672924, 2.904280683598008839, -5.030361703432631337 ) ) ;
#11812=CARTESIAN_POINT ( 'NONE',  ( 0.4465819873852032162, 5.773502691896260863, 3.074436065535979155E-16 ) ) ;
#11822=( GEOMETRIC_REPRESENTATION_CONTEXT ( 3 ) GLOBAL_UNCERTAINTY_ASSIGNED_CONTEXT ( ( #14315 ) ) GLOBAL_UNIT_ASSIGNED_CONTEXT ( ( #2373, #9025, #11382 ) ) REPRESENTATION_CONTEXT ( 'NONE', 'WORKASPACE' ) );
#11843=EDGE_LOOP ( 'NONE', ( #14597, #135, #13692, #14190, #4553 ) ) ;
#11864=CARTESIAN_POINT ( 'NONE',  ( 0.1983443223721549353, -3.359771601077103487, 4.180704885107415336 ) ) ;
#11868=CARTESIAN_POINT ( 'NONE',  ( 6.244297270354684848, -1.799661607120071246E-11, -5.105276777067894400 ) ) ;
#11869=CARTESIAN_POINT ( 'NONE',  ( 6.244004651191001010, 4.178905357954649347, -2.972460101650455488 ) ) ;
#11876=CARTESIAN_POINT ( 'NONE',  ( 6.207671477328696952, 3.321994320370140752, -4.246137054663666532 ) ) ;
#11886=ORIENTED_EDGE ( 'NONE', *, *, #6239, .T. ) ;
#11892=ORIENTED_EDGE ( 'NONE', *, *, #427, .F. ) ;
#11910=CARTESIAN_POINT ( 'NONE',  ( 6.357976367242104132, -3.426708043488309041, 4.282301071215474764 ) ) ;
#11931=CARTESIAN_POINT ( 'NONE',  ( 6.244297270354683960, 1.800816419761795034E-11, 5.105276777067893512 ) ) ;
#11939=UNCERTAINTY_MEASURE_WITH_UNIT (LENGTH_MEASURE( 1.000000000000000082E-05 ), #4163, 'distance_accuracy_value', 'NONE');
#11942=DIRECTION ( 'NONE',  ( -1.000000000000000000, 0.000000000000000000, -0.000000000000000000 ) ) ;
#11995=STYLED_ITEM('',(#14681),#7073);
#12010=CARTESIAN_POINT ( 'NONE',  ( 6.244889965166094292, 3.924082311521017274, 3.413878157001050795 ) ) ;
#12025=CARTESIAN_POINT ( 'NONE',  ( 6.196878017913833858, -1.924500897298760727, -5.000000000000000888 ) ) ;
#12055=CARTESIAN_POINT ( 'NONE',  ( 0.3106000600989257121, 3.122278952918442485, -4.592054218142294530 ) ) ;
#12059=AXIS2_PLACEMENT_3D ( 'NONE', #14053, #4904, #3654 ) ;
#12069=EDGE_CURVE ( 'NONE', #9255, #10781, #13179, .T. ) ;
#12095=CARTESIAN_POINT ( 'NONE',  ( 6.362374563308399900, 5.433808049140282037, -0.8060918076007316246 ) ) ;
#12103=CARTESIAN_POINT ( 'NONE',  ( 6.367873360227555679, -2.886751345948120662, 4.999999999999999112 ) ) ;
#12131=CARTESIAN_POINT ( 'NONE',  ( 6.242800618755127928, -3.923709308887747937, 3.414402460853335874 ) ) ;
#12174=DIRECTION ( 'NONE',  ( 0.000000000000000000, 0.000000000000000000, 1.000000000000000000 ) ) ;
#12205=CARTESIAN_POINT ( 'NONE',  ( 8.500000000000000000, -5.773502691896264416, 0.000000000000000000 ) ) ;
#12210=CARTESIAN_POINT ( 'NONE',  ( 7.336184427528458230, 0.000000000000000000, 0.000000000000000000 ) ) ;
#12239=AXIS2_PLACEMENT_3D ( 'NONE', #1216, #5722, #12282 ) ;
#12247=CIRCLE ( 'NONE', #8245, 5.000000000000000000 ) ;
#12282=DIRECTION ( 'NONE',  ( 0.000000000000000000, 0.000000000000000000, 1.000000000000000000 ) ) ;
#12285=DIRECTION ( 'NONE',  ( 0.000000000000000000, 0.000000000000000000, -1.000000000000000000 ) ) ;
#12294=CARTESIAN_POINT ( 'NONE',  ( 6.271006797790669829, 0.9853839345309236553, 5.106080050406710313 ) ) ;
#12297=DIRECTION ( 'NONE',  ( 0.000000000000000000, 0.000000000000000000, 1.000000000000000000 ) ) ;
#12298=AXIS2_PLACEMENT_3D ( 'NONE', #1472, #6774, #2568 ) ;
#12300=CARTESIAN_POINT ( 'NONE',  ( 6.371506350351446635, 5.409331239960136983, 0.8483282427581467777 ) ) ;
#12312=EDGE_CURVE ( 'NONE', #6891, #9255, #12903, .T. ) ;
#12317=DIRECTION ( 'NONE',  ( 0.3420201433256622736, 0.000000000000000000, -0.9396926207859106484 ) ) ;
#12341=ORIENTED_EDGE ( 'NONE', *, *, #106, .F. ) ;
#12363=DIRECTION ( 'NONE',  ( 0.000000000000000000, 0.000000000000000000, 1.000000000000000000 ) ) ;
#12398=DIRECTION ( 'NONE',  ( -1.000000000000000000, -0.000000000000000000, -0.000000000000000000 ) ) ;
#12411=B_SPLINE_CURVE_WITH_KNOTS ( 'NONE', 3,
 ( #6330, #13488, #13622, #1230, #7807, #14519 ),
 .UNSPECIFIED., .F., .F.,
 ( 4, 2, 4 ),
 ( 0.008261945092156346496, 0.009724140865920691962, 0.01118633663968503569 ),
 .UNSPECIFIED. ) ;
#12424=DIRECTION ( 'NONE',  ( 0.000000000000000000, 0.8660254037844375974, -0.5000000000000018874 ) ) ;
#12447=DIRECTION ( 'NONE',  ( 0.000000000000000000, 0.000000000000000000, -1.000000000000000000 ) ) ;
#12449=CARTESIAN_POINT ( 'NONE',  ( 6.367873360227559232, -5.773502691896264416, 0.000000000000000000 ) ) ;
#12457=DIRECTION ( 'NONE',  ( 0.000000000000000000, 0.000000000000000000, -1.000000000000000000 ) ) ;
#12471=DIRECTION ( 'NONE',  ( 0.000000000000000000, 0.000000000000000000, -1.000000000000000000 ) ) ;
#12487=CARTESIAN_POINT ( 'NONE',  ( 6.212068001623188174, 5.350125758160983125, -0.7333103599822197172 ) ) ;
#12501=ORIENTED_EDGE ( 'NONE', *, *, #10772, .F. ) ;
#12516=CARTESIAN_POINT ( 'NONE',  ( 8.500000000000000000, 0.000000000000000000, 4.000000000000000000 ) ) ;
#12528=CIRCLE ( 'NONE', #9483, 4.000000000000000000 ) ;
#12537=DIRECTION ( 'NONE',  ( 0.000000000000000000, 0.000000000000000000, -1.000000000000000000 ) ) ;
#12552=CARTESIAN_POINT ( 'NONE',  ( 6.367873360227556567, 2.886751345948122882, -5.000000000000000000 ) ) ;
#12604=CARTESIAN_POINT ( 'NONE',  ( 0.000000000000000000, -4.330127018922189208, 2.500000000000010658 ) ) ;
#12606=EDGE_LOOP ( 'NONE', ( #3418, #3884, #11892, #10226, #7259, #11211 ) ) ;
#12608=DIRECTION ( 'NONE',  ( 0.000000000000000000, -1.000000000000000000, 0.000000000000000000 ) ) ;
#12612=CARTESIAN_POINT ( 'NONE',  ( 6.534838248920899595, -2.951765777552421532, -5.112608298763837489 ) ) ;
#12637=CARTESIAN_POINT ( 'NONE',  ( 6.212068001622437663, 3.310128279683251851, 4.266689640018040741 ) ) ;
#12642=CARTESIAN_POINT ( 'NONE',  ( 6.527192678185238961, 5.883244248022512224, -1.510895765055974796E-13 ) ) ;
#12674=CARTESIAN_POINT ( 'NONE',  ( 0.4465819873851995525, 2.886751345948122882, -5.000000000000000000 ) ) ;
#12701=CARTESIAN_POINT ( 'NONE',  ( 0.05140428708382614731, 4.819072548984002502, 1.653121499799249161 ) ) ;
#12705=CARTESIAN_POINT ( 'NONE',  ( 6.452281807715710471, 2.898928808473055341, 5.021091983800445746 ) ) ;
#12716=CARTESIAN_POINT ( 'NONE',  ( 8.500000000000000000, 0.000000000000000000, 0.000000000000000000 ) ) ;
#12727=ORIENTED_EDGE ( 'NONE', *, *, #6923, .T. ) ;
#12759=CARTESIAN_POINT ( 'NONE',  ( 0.05140428708382493994, -3.841181488860375026, 3.346878500200758833 ) ) ;
#12763=AXIS2_PLACEMENT_3D ( 'NONE', #9609, #8280, #12859 ) ;
#12764=CARTESIAN_POINT ( 'NONE',  ( 6.445127866599362321, 3.194847394660946804, -4.687657648742338701 ) ) ;
#12772=CARTESIAN_POINT ( 'NONE',  ( 6.534533895392293346, -2.951347675328725995, 5.111884124469654900 ) ) ;
#12777=CARTESIAN_POINT ( 'NONE',  ( 0.000000000000000000, -4.330127018922189208, 2.500000000000010658 ) ) ;
#12784=CARTESIAN_POINT ( 'NONE',  ( 6.481779955677544613, 2.910222513313213799, 5.040653254389286353 ) ) ;
#12791=EDGE_CURVE ( 'NONE', #12984, #10586, #3863, .T. ) ;
#12830=CARTESIAN_POINT ( 'NONE',  ( 0.08165819712377203610, -4.939961795957301227, -1.443735181952766400 ) ) ;
#12859=DIRECTION ( 'NONE',  ( 0.000000000000000000, -0.5000000000000001110, 0.8660254037844387076 ) ) ;
#12888=ADVANCED_FACE ( 'NONE', ( #1710 ), #14187, .F. ) ;
#12890=CARTESIAN_POINT ( 'NONE',  ( 6.533910050139694725, 2.950514251728030946, -5.110440592449080555 ) ) ;
#12901=CONICAL_SURFACE ( 'NONE', #5133, 8.105212085995399107, 1.221730476396037490 ) ;
#12903=LINE ( 'NONE', #8323, #13683 ) ;
#12922=CARTESIAN_POINT ( 'NONE',  ( 0.3106000600989282101, 5.537975084925940372, 0.4079457818577104100 ) ) ;
#12968=EDGE_CURVE ( 'NONE', #14024, #13548, #8707, .T. ) ;
#12978=EDGE_CURVE ( 'NONE', #14024, #11464, #399, .T. ) ;
#12984=VERTEX_POINT ( 'NONE', #3402 ) ;
#12985=CARTESIAN_POINT ( 'NONE',  ( 6.270568613849415662, 3.932080789230358420, -3.401571648088638433 ) ) ;
#12999=DIRECTION ( 'NONE',  ( 1.000000000000000000, 0.000000000000000000, -0.000000000000000000 ) ) ;
#13020=DIRECTION ( 'NONE',  ( 0.000000000000000000, 0.000000000000000000, -1.000000000000000000 ) ) ;
#13040=CARTESIAN_POINT ( 'NONE',  ( 6.362374563308329734, -5.433808049140088414, 0.8060918076006072797 ) ) ;
#13043=CARTESIAN_POINT ( 'NONE',  ( 7.336184427528458230, 0.000000000000000000, 0.000000000000000000 ) ) ;
#13062=EDGE_CURVE ( 'NONE', #13338, #5340, #1852, .T. ) ;
#13137=PRODUCT_DEFINITION_CONTEXT ( 'detailed design', #14332, 'design' ) ;
#13138=DIRECTION ( 'NONE',  ( -1.000000000000000000, -0.000000000000000000, -0.000000000000000000 ) ) ;
#13154=EDGE_CURVE ( 'NONE', #3784, #12984, #4478, .T. ) ;
#13163=ORIENTED_EDGE ( 'NONE', *, *, #14466, .T. ) ;
#13179=LINE ( 'NONE', #693, #9020 ) ;
#13200=CARTESIAN_POINT ( 'NONE',  ( 6.270568613849413886, 4.911887854652841057, 1.704496029161937320 ) ) ;
#13217=DIRECTION ( 'NONE',  ( 0.000000000000000000, 0.000000000000000000, -1.000000000000000000 ) ) ;
#13218=CARTESIAN_POINT ( 'NONE',  ( 6.445127866599366762, -5.657054305385778470, -0.4229901806197434722 ) ) ;
#13233=B_SPLINE_CURVE_WITH_KNOTS ( 'NONE', 3,
 ( #500, #8247, #13948, #12759, #3842, #11864, #6118, #1536 ),
 .UNSPECIFIED., .F., .F.,
 ( 4, 2, 2, 4 ),
 ( 0.002921158011986728538, 0.003648658599403080925, 0.004376159186819432445, 0.005831160361652135485 ),
 .UNSPECIFIED. ) ;
#13255=CARTESIAN_POINT ( 'NONE',  ( 6.541171661047877173, -5.920857802016178617, -0.02973393389964841538 ) ) ;
#13267=DIRECTION ( 'NONE',  ( 0.000000000000000000, 0.000000000000000000, -1.000000000000000000 ) ) ;
#13286=ORIENTED_EDGE ( 'NONE', *, *, #106, .T. ) ;
#13314=ADVANCED_FACE ( 'NONE', ( #11670 ), #13659, .T. ) ;
#13317=CARTESIAN_POINT ( 'NONE',  ( 6.095473853218515536, -4.853892138986623195, 1.592812200815997725 ) ) ;
#13327=ORIENTED_EDGE ( 'NONE', *, *, #4390, .T. ) ;
#13333=DIRECTION ( 'NONE',  ( -0.000000000000000000, 0.000000000000000000, -1.000000000000000000 ) ) ;
#13334=DIRECTION ( 'NONE',  ( -1.000000000000000000, -0.000000000000000000, -0.000000000000000000 ) ) ;
#13338=VERTEX_POINT ( 'NONE', #592 ) ;
#13351=CARTESIAN_POINT ( 'NONE',  ( 0.000000000000000000, 0.000000000000000000, 0.000000000000000000 ) ) ;
#13352=CARTESIAN_POINT ( 'NONE',  ( 0.000000000000000000, 0.000000000000000000, 0.000000000000000000 ) ) ;
#13360=CARTESIAN_POINT ( 'NONE',  ( 43.50000000000000711, 0.000000000000000000, 0.000000000000000000 ) ) ;
#13369=SHAPE_REPRESENTATION_RELATIONSHIP ( 'NONE' , 'NONE' ,  #9337, #4067 ) ;
#13384=DIRECTION ( 'NONE',  ( 1.000000000000000000, 0.000000000000000000, -0.000000000000000000 ) ) ;
#13393=CARTESIAN_POINT ( 'NONE',  ( 0.000000000000000000, 4.330127018922190985, -2.500000000000007105 ) ) ;
#13399=EDGE_CURVE ( 'NONE', #483, #9509, #4270, .T. ) ;
#13401=CARTESIAN_POINT ( 'NONE',  ( 0.4465819873851989974, -2.886751345948121106, 4.999999999999999112 ) ) ;
#13446=EDGE_LOOP ( 'NONE', ( #2349, #6825, #9148, #8340, #5922 ) ) ;
#13474=PRODUCT ( 'hex flange bolt small_iso_ISO 4162 - M8 x 35 x 22-N', 'hex flange bolt small_iso_ISO 4162 - M8 x 35 x 22-N', '', ( #737 ) ) ;
#13479=ORIENTED_EDGE ( 'NONE', *, *, #14608, .T. ) ;
#13480=DIRECTION ( 'NONE',  ( 0.000000000000000000, 0.5000000000000018874, 0.8660254037844375974 ) ) ;
#13481=ORIENTED_EDGE ( 'NONE', *, *, #7164, .F. ) ;
#13483=CARTESIAN_POINT ( 'NONE',  ( 0.000000000000000000, -4.330127018922194537, -2.500000000000000444 ) ) ;
#13488=CARTESIAN_POINT ( 'NONE',  ( -1.059638217015129330E-15, 0.4887495715076925484, 4.999999999999999112 ) ) ;
#13490=CARTESIAN_POINT ( 'NONE',  ( 5.991014884144048480, 2.818925648462311528E-15, 4.999999999999999112 ) ) ;
#13513=CARTESIAN_POINT ( 'NONE',  ( 6.533910050139697390, -5.901028503456124952, 6.252275320486994560E-15 ) ) ;
#13522=DIRECTION ( 'NONE',  ( -1.000000000000000000, -0.000000000000000000, -0.000000000000000000 ) ) ;
#13530=FILL_AREA_STYLE_COLOUR ( '', #1934 ) ;
#13548=VERTEX_POINT ( 'NONE', #13708 ) ;
#13556=CARTESIAN_POINT ( 'NONE',  ( 6.367873360227555679, -2.886751345948120662, 4.999999999999999112 ) ) ;
#13571=ORIENTED_EDGE ( 'NONE', *, *, #3766, .T. ) ;
#13574=CARTESIAN_POINT ( 'NONE',  ( 6.452281807715713136, -5.797857616946124892, 1.707831949354040044E-16 ) ) ;
#13588=CARTESIAN_POINT ( 'NONE',  ( 6.541171661047876285, -2.934678558896549383, -5.142480235691125223 ) ) ;
#13605=PLANE ( 'NONE',  #11585 ) ;
#13616=VECTOR ( 'NONE', #12317, 1000.000000000000114 ) ;
#13622=CARTESIAN_POINT ( 'NONE',  ( 0.04320752586819773255, 0.9836842030436150353, 4.999999999999999112 ) ) ;
#13659=CONICAL_SURFACE ( 'NONE', #9180, 5.000000000000000888, 1.047197551196600296 ) ;
#13683=VECTOR ( 'NONE', #6034, 999.9999999999998863 ) ;
#13690=CIRCLE ( 'NONE', #9458, 5.000000000000000888 ) ;
#13692=ORIENTED_EDGE ( 'NONE', *, *, #12791, .T. ) ;
#13696=ORIENTED_EDGE ( 'NONE', *, *, #13154, .T. ) ;
#13698=CARTESIAN_POINT ( 'NONE',  ( 6.245813541929282842, 1.036329910263561471, -5.105320956836709279 ) ) ;
#13708=CARTESIAN_POINT ( 'NONE',  ( 6.534838248920899595, -2.951765777552421532, -5.112608298763837489 ) ) ;
#13724=CIRCLE ( 'NONE', #5477, 0.5999999999999980904 ) ;
#13732=CARTESIAN_POINT ( 'NONE',  ( 6.495567275914607031, -5.834887664330119961, -8.422077706216564275E-17 ) ) ;
#13737=CARTESIAN_POINT ( 'NONE',  ( 6.245835795331710294, -1.036512332922514767, 5.105321605219339531 ) ) ;
#13756=ADVANCED_FACE ( 'NONE', ( #5957 ), #11472, .F. ) ;
#13778=EDGE_LOOP ( 'NONE', ( #14423, #4875 ) ) ;
#13797=CARTESIAN_POINT ( 'NONE',  ( 43.50000000000000711, 4.052968581778165278E-16, -3.309499999999999886 ) ) ;
#13799=ORIENTED_EDGE ( 'NONE', *, *, #7077, .T. ) ;
#13804=CARTESIAN_POINT ( 'NONE',  ( 6.541171370350062020, -2.986177670315871335, 5.112746295475706582 ) ) ;
#13816=CARTESIAN_POINT ( 'NONE',  ( 6.466260427357663154, 2.904280683598005730, 5.030361703432624232 ) ) ;
#13820=FACE_OUTER_BOUND ( 'NONE', #9916, .T. ) ;
#13861=CARTESIAN_POINT ( 'NONE',  ( 0.01055556052339231068, -4.575665857285986959, -2.074714256722481220 ) ) ;
#13867=CARTESIAN_POINT ( 'NONE',  ( 6.534838248920899595, 5.903531555104835071, -2.091255385257999292E-17 ) ) ;
#13892=CARTESIAN_POINT ( 'NONE',  ( 6.506987859255518813, 2.925375531177291766, 5.066899051217865768 ) ) ;
#13900=AXIS2_PLACEMENT_3D ( 'NONE', #5437, #2094, #1060 ) ;
#13932=CARTESIAN_POINT ( 'NONE',  ( 6.270568613849412998, -3.932080789230356643, 3.401571648088637101 ) ) ;
#13948=CARTESIAN_POINT ( 'NONE',  ( 0.01055556052338863481, -4.084588180558399451, 2.925285743277528105 ) ) ;
#13961=CARTESIAN_POINT ( 'NONE',  ( 6.385552186430388133, -2.886751345948119329, 5.000000000000000888 ) ) ;
#13990=CARTESIAN_POINT ( 'NONE',  ( 43.50000000000000711, 0.000000000000000000, 0.000000000000000000 ) ) ;
#14004=CARTESIAN_POINT ( 'NONE',  ( 0.04320752586819841951, 0.9836842030436123707, -5.000000000000000000 ) ) ;
#14024=VERTEX_POINT ( 'NONE', #7788 ) ;
#14039=( BOUNDED_SURFACE ( )  B_SPLINE_SURFACE ( 3, 2, ( 
 ( #11236, #11314, #3493 ),
 ( #12487, #2385, #12095 ),
 ( #4205, #14250, #4072 ),
 ( #8630, #6344, #5100 ),
 ( #11876, #8565, #7449 ),
 ( #10704, #5316, #3989 ) ),
 .UNSPECIFIED., .F., .F., .F. ) 
 B_SPLINE_SURFACE_WITH_KNOTS ( ( 4, 2, 4 ),
 ( 3, 3 ),
 ( 0.02367865728600888550, 0.02663179453327094853, 0.02958493178053300809 ),
 ( 0.000000000000000000, 1.000000000000000000 ),
 .UNSPECIFIED. ) 
 GEOMETRIC_REPRESENTATION_ITEM ( )  RATIONAL_B_SPLINE_SURFACE ( (
 ( 1.000000000000000000, 0.8047781103519414669, 1.000000000000000000),
 ( 1.000000000000000000, 0.8123785825980049946, 1.000000000000000000),
 ( 1.000000000000000000, 0.8190671539288042480, 1.000000000000000000),
 ( 1.000000000000000000, 0.8192352255335092481, 1.000000000000000000),
 ( 1.000000000000000000, 0.8126129676835899263, 1.000000000000000000),
 ( 1.000000000000000000, 0.8047712537969735624, 1.000000000000000000) ) ) 
 REPRESENTATION_ITEM ( '' )  SURFACE ( )  );
#14043=CARTESIAN_POINT ( 'NONE',  ( 6.385552186430388133, 2.886751345948125547, 4.999999999999999112 ) ) ;
#14053=CARTESIAN_POINT ( 'NONE',  ( 0.000000000000000000, 0.000000000000000000, 0.000000000000000000 ) ) ;
#14066=CARTESIAN_POINT ( 'NONE',  ( -5.065257024580716028E-16, 0.4887495715076925484, -5.000000000000000000 ) ) ;
#14174=CONICAL_SURFACE ( 'NONE', #1439, 5.000000000000000888, 1.047197551196600296 ) ;
#14187=PLANE ( 'NONE',  #11051 ) ;
#14190=ORIENTED_EDGE ( 'NONE', *, *, #9016, .F. ) ;
#14218=EDGE_LOOP ( 'NONE', ( #5246, #9382, #8834, #9776, #8146 ) ) ;
#14227=CLOSED_SHELL ( 'NONE', ( #14399, #9083, #1696, #5678, #11205, #7621, #3592, #13756, #6003, #1023, #10757, #14353, #1874, #13314, #401, #7626, #8667, #12888, #9355, #8729, #1849, #7733, #7467, #11101, #318, #8546, #8801, #3447, #5057 ) ) ;
#14232=ORIENTED_EDGE ( 'NONE', *, *, #427, .T. ) ;
#14237=VERTEX_POINT ( 'NONE', #3879 ) ;
#14245=EDGE_LOOP ( 'NONE', ( #13286, #6961, #14355, #7589 ) ) ;
#14250=CARTESIAN_POINT ( 'NONE',  ( 6.207530437345012864, 4.849805425594809094, -1.599890596046773084 ) ) ;
#14263=CARTESIAN_POINT ( 'NONE',  ( 8.500000000000000000, 4.898587196589412829E-16, -4.000000000000000000 ) ) ;
#14267=B_SPLINE_CURVE_WITH_KNOTS ( 'NONE', 3,
 ( #4215, #2131, #4144, #12025, #803 ),
 .UNSPECIFIED., .F., .F.,
 ( 4, 1, 4 ),
 ( 0.000000000000000000, 0.002886751345948128985, 0.005773502691896257970 ),
 .UNSPECIFIED. ) ;
#14279=CARTESIAN_POINT ( 'NONE',  ( 0.4465819873851995525, 2.886751345948122882, -5.000000000000000000 ) ) ;
#14282=ORIENTED_EDGE ( 'NONE', *, *, #5240, .F. ) ;
#14302=DIRECTION ( 'NONE',  ( 0.000000000000000000, 0.000000000000000000, 1.000000000000000000 ) ) ;
#14315=UNCERTAINTY_MEASURE_WITH_UNIT (LENGTH_MEASURE( 1.000000000000000082E-05 ), #2373, 'distance_accuracy_value', 'NONE');
#14331=CARTESIAN_POINT ( 'NONE',  ( 6.507056315241515954, 5.826803161468471437, -0.09231912136634902455 ) ) ;
#14332=APPLICATION_CONTEXT ( 'automotive_design' ) ;
#14346=CARTESIAN_POINT ( 'NONE',  ( 0.01055556052338848388, 4.084588180558401227, -2.925285743277528550 ) ) ;
#14352=B_SPLINE_CURVE_WITH_KNOTS ( 'NONE', 3,
 ( #3674, #3899, #2642, #10524 ),
 .UNSPECIFIED., .F., .F.,
 ( 4, 4 ),
 ( 2.380735200829041677E-07, 0.002921158011986708155 ),
 .UNSPECIFIED. ) ;
#14353=ADVANCED_FACE ( 'NONE', ( #5119 ), #14390, .T. ) ;
#14355=ORIENTED_EDGE ( 'NONE', *, *, #10760, .F. ) ;
#14388=CARTESIAN_POINT ( 'NONE',  ( 8.500000000000000000, 0.000000000000000000, 0.000000000000000000 ) ) ;
#14390=CONICAL_SURFACE ( 'NONE', #4261, 5.000000000000000888, 1.047197551196600296 ) ;
#14399=ADVANCED_FACE ( 'NONE', ( #1787 ), #9207, .T. ) ;
#14411=PRODUCT_DEFINITION_SHAPE ( 'NONE', 'NONE',  #4059 ) ;
#14423=ORIENTED_EDGE ( 'NONE', *, *, #5240, .T. ) ;
#14441=ORIENTED_EDGE ( 'NONE', *, *, #10616, .T. ) ;
#14448=FACE_OUTER_BOUND ( 'NONE', #6254, .T. ) ;
#14449=VERTEX_POINT ( 'NONE', #1166 ) ;
#14451=DIRECTION ( 'NONE',  ( 1.000000000000000000, 0.000000000000000000, -0.000000000000000000 ) ) ;
#14452=FACE_OUTER_BOUND ( 'NONE', #7194, .T. ) ;
#14466=EDGE_CURVE ( 'NONE', #6264, #483, #5750, .T. ) ;
#14482=CARTESIAN_POINT ( 'NONE',  ( 6.244297270354684848, -1.799661607120071246E-11, -5.105276777067894400 ) ) ;
#14514=VERTEX_POINT ( 'NONE', #9220 ) ;
#14519=CARTESIAN_POINT ( 'NONE',  ( 0.4465819873851997746, 2.886751345948125547, 4.999999999999999112 ) ) ;
#14535=ORIENTED_EDGE ( 'NONE', *, *, #7954, .T. ) ;
#14537=CARTESIAN_POINT ( 'NONE',  ( 6.534838248920900483, -5.903531555104837736, 5.201568163584232486E-16 ) ) ;
#14576=AXIS2_PLACEMENT_3D ( 'NONE', #8963, #7789, #9933 ) ;
#14583=CARTESIAN_POINT ( 'NONE',  ( 0.1739375980333479899, -3.358985280702904586, -4.182066831946573693 ) ) ;
#14597=ORIENTED_EDGE ( 'NONE', *, *, #1765, .F. ) ;
#14608=EDGE_CURVE ( 'NONE', #5340, #10297, #13233, .T. ) ;
#14675=COLOUR_RGB('Black',0.12,0.14,0.17);
#14676=FILL_AREA_STYLE_COLOUR('',#14675);
#14677=FILL_AREA_STYLE('',(#14676));
#14678=SURFACE_STYLE_FILL_AREA(#14677);
#14679=SURFACE_SIDE_STYLE('',(#14678));
#14680=SURFACE_STYLE_USAGE(.BOTH.,#14679);
#14681=PRESENTATION_STYLE_ASSIGNMENT((#14680));
ENDSEC;
END-ISO-10303-21;
